ISO-10303-21;
HEADER;
FILE_DESCRIPTION (('STEP AP214'),
    '1' );
FILE_NAME ('Attachment Screw.step',
    '2026-10-09T09:51:18',
    ( '' ),
    ( '' ),
    'SwSTEP 2.0',
    'SolidWorks 2026',
    '' );
FILE_SCHEMA (( 'AUTOMOTIVE_DESIGN' ));
ENDSEC;

DATA;
#42=CARTESIAN_POINT ( 'NONE',  ( -45.46395726858714426, -13.72754205882879042, 70.13000000000000966 ) ) ;
#49=ORIENTED_EDGE ( 'NONE', *, *, #23162, .T. ) ;
#73=VERTEX_POINT ( 'NONE', #14975 ) ;
#78=ADVANCED_FACE ( 'NONE', ( #20432 ), #5892, .T. ) ;
#93=VERTEX_POINT ( 'NONE', #9602 ) ;
#118=DIRECTION ( 'NONE',  ( 0.000000000000000000, 0.000000000000000000, 1.000000000000000000 ) ) ;
#131=DIRECTION ( 'NONE',  ( -0.4461977533475101620, -0.8949343913984054710, 1.541409258166069499E-16 ) ) ;
#132=AXIS2_PLACEMENT_3D ( 'NONE', #40046, #2613, #47672 ) ;
#184=CARTESIAN_POINT ( 'NONE',  ( -45.92409385541306222, -14.20920654474410760, 70.50000000000000000 ) ) ;
#233=ORIENTED_EDGE ( 'NONE', *, *, #20231, .T. ) ;
#289=DIRECTION ( 'NONE',  ( 1.224646799147353207E-16, 1.000000000000000000, -1.912410701131276611E-32 ) ) ;
#341=ORIENTED_EDGE ( 'NONE', *, *, #46783, .F. ) ;
#391=ORIENTED_EDGE ( 'NONE', *, *, #42461, .T. ) ;
#422=EDGE_LOOP ( 'NONE', ( #46320, #35435, #35647 ) ) ;
#434=ORIENTED_EDGE ( 'NONE', *, *, #20231, .F. ) ;
#461=DIRECTION ( 'NONE',  ( -1.224646799147353207E-16, -1.000000000000000000, 1.912410701131276611E-32 ) ) ;
#718=AXIS2_PLACEMENT_3D ( 'NONE', #30330, #289, #34963 ) ;
#754=DIRECTION ( 'NONE',  ( 0.4461977533473615032, -0.8949343913984796339, 0.000000000000000000 ) ) ;
#791=VECTOR ( 'NONE', #36841, 1000.000000000000000 ) ;
#856=CIRCLE ( 'NONE', #26795, 3.982850737850967437 ) ;
#927=ORIENTED_EDGE ( 'NONE', *, *, #45982, .T. ) ;
#957=ORIENTED_EDGE ( 'NONE', *, *, #17972, .F. ) ;
#963=CARTESIAN_POINT ( 'NONE',  ( -46.46711114793018282, -12.76354662275040219, 70.13000000000000966 ) ) ;
#982=DIRECTION ( 'NONE',  ( 0.000000000000000000, 0.000000000000000000, 1.000000000000000000 ) ) ;
#1097=DIRECTION ( 'NONE',  ( 1.000000000000000000, -1.224646799147353207E-16, 3.142942573426604379E-15 ) ) ;
#1099=( BOUNDED_CURVE ( )  B_SPLINE_CURVE ( 3, ( #48352, #40977, #26204, #14838 ),
 .UNSPECIFIED., .F., .F. ) 
 B_SPLINE_CURVE_WITH_KNOTS ( ( 4, 4 ),
 ( 6.147240100463230661, 6.419130513895940915 ),
 .UNSPECIFIED. ) 
 CURVE ( )  GEOMETRIC_REPRESENTATION_ITEM ( )  RATIONAL_B_SPLINE_CURVE ( ( 1.000000000000000000, 0.9938491152761211866, 0.9938491152761211866, 1.000000000000000000 ) ) 
 REPRESENTATION_ITEM ( '' )  );
#1127=ORIENTED_EDGE ( 'NONE', *, *, #22561, .T. ) ;
#1138=AXIS2_PLACEMENT_3D ( 'NONE', #47596, #28869, #48300 ) ;
#1184=FACE_OUTER_BOUND ( 'NONE', #31912, .T. ) ;
#1207=CARTESIAN_POINT ( 'NONE',  ( -45.38107656289594161, -12.76354662275040219, 70.13000000000000966 ) ) ;
#1289=EDGE_CURVE ( 'NONE', #45322, #16774, #44431, .T. ) ;
#1306=CARTESIAN_POINT ( 'NONE',  ( -45.92409385541306222, -14.20920654474410760, 70.50000000000000000 ) ) ;
#1315=CARTESIAN_POINT ( 'NONE',  ( -46.29409385541305255, -14.20920654474410760, 70.08498674719956512 ) ) ;
#1417=AXIS2_PLACEMENT_3D ( 'NONE', #25171, #21234, #33249 ) ;
#1450=CARTESIAN_POINT ( 'NONE',  ( -45.92409385541306222, -13.70421070448076861, 68.24000000000000909 ) ) ;
#1480=AXIS2_PLACEMENT_3D ( 'NONE', #39435, #35962, #6664 ) ;
#1524=( BOUNDED_CURVE ( )  B_SPLINE_CURVE ( 3, ( #46875, #31367, #46397, #42710 ),
 .UNSPECIFIED., .F., .F. ) 
 B_SPLINE_CURVE_WITH_KNOTS ( ( 4, 4 ),
 ( 2.926239601924445180E-15, 0.1359452067163722244 ),
 .UNSPECIFIED. ) 
 CURVE ( )  GEOMETRIC_REPRESENTATION_ITEM ( )  RATIONAL_B_SPLINE_CURVE ( ( 1.000000000000000000, 0.9984605012767909793, 0.9984605012767909793, 1.000000000000000000 ) ) 
 REPRESENTATION_ITEM ( '' )  );
#1551=ORIENTED_EDGE ( 'NONE', *, *, #20178, .T. ) ;
#1555=CARTESIAN_POINT ( 'NONE',  ( -45.46395726858714426, -13.72754205882879042, 70.87000000000000455 ) ) ;
#1571=VERTEX_POINT ( 'NONE', #21228 ) ;
#1581=AXIS2_PLACEMENT_3D ( 'NONE', #30557, #11835, #11343 ) ;
#1658=AXIS2_PLACEMENT_3D ( 'NONE', #41245, #48147, #22290 ) ;
#1671=UNCERTAINTY_MEASURE_WITH_UNIT (LENGTH_MEASURE( 1.000000000000000082E-05 ), #47548, 'distance_accuracy_value', 'NONE');
#1707=DIRECTION ( 'NONE',  ( 0.000000000000000000, 1.000000000000000000, 0.000000000000000000 ) ) ;
#1761=ORIENTED_EDGE ( 'NONE', *, *, #21839, .T. ) ;
#1971=ADVANCED_FACE ( 'NONE', ( #17463 ), #13751, .T. ) ;
#2023=LINE ( 'NONE', #47089, #10124 ) ;
#2072=LINE ( 'NONE', #10448, #14918 ) ;
#2084=AXIS2_PLACEMENT_3D ( 'NONE', #2444, #35672, #25098 ) ;
#2125=VERTEX_POINT ( 'NONE', #47160 ) ;
#2149=CONICAL_SURFACE ( 'NONE', #9230, 0.5560000000000009379, 0.06981317007976595157 ) ;
#2184=CIRCLE ( 'NONE', #19484, 0.5560000000000009379 ) ;
#2304=CIRCLE ( 'NONE', #42420, 0.5560000000000009379 ) ;
#2305=DIRECTION ( 'NONE',  ( 1.000000000000000000, 0.000000000000000000, 0.000000000000000000 ) ) ;
#2315=EDGE_CURVE ( 'NONE', #7630, #37913, #1099, .T. ) ;
#2317=CARTESIAN_POINT ( 'NONE',  ( -45.92409385541306932, -12.76354662275040042, 70.50000000000000000 ) ) ;
#2340=CARTESIAN_POINT ( 'NONE',  ( -45.55409385541305767, -12.91120565595569936, 69.30071302485083606 ) ) ;
#2391=DIRECTION ( 'NONE',  ( 4.267285103686815209E-17, -5.292884291094200710E-16, -1.000000000000000000 ) ) ;
#2444=CARTESIAN_POINT ( 'NONE',  ( -45.92409385541306222, -14.80920654474410725, 70.50000000000000000 ) ) ;
#2527=CARTESIAN_POINT ( 'NONE',  ( -45.92409385541293432, 985.6101381041504510, 70.50000000000000000 ) ) ;
#2550=ORIENTED_EDGE ( 'NONE', *, *, #17972, .T. ) ;
#2591=EDGE_CURVE ( 'NONE', #45017, #39895, #35194, .T. ) ;
#2613=DIRECTION ( 'NONE',  ( 1.224646799147353207E-16, 1.000000000000000000, -1.912410701131276611E-32 ) ) ;
#2640=EDGE_CURVE ( 'NONE', #7134, #16837, #13761, .T. ) ;
#2714=PRESENTATION_STYLE_ASSIGNMENT (( #28354 ) ) ;
#2786=DIRECTION ( 'NONE',  ( -5.551115123125782702E-17, -1.232595164407830946E-32, -1.000000000000000000 ) ) ;
#2826=ORIENTED_EDGE ( 'NONE', *, *, #17243, .F. ) ;
#2883=AXIS2_PLACEMENT_3D ( 'NONE', #34307, #45903, #11425 ) ;
#2896=DIRECTION ( 'NONE',  ( -3.534154189880001717E-15, 4.519331686442879103E-31, 1.000000000000000000 ) ) ;
#2912=ORIENTED_EDGE ( 'NONE', *, *, #3392, .T. ) ;
#2984=CARTESIAN_POINT ( 'NONE',  ( -46.29409385541305255, -13.24559821555319061, 71.00222776205100672 ) ) ;
#2990=ORIENTED_EDGE ( 'NONE', *, *, #29440, .T. ) ;
#2998=CARTESIAN_POINT ( 'NONE',  ( -45.55409385541305767, -12.76354662275040219, 69.95698270748289360 ) ) ;
#3093=LINE ( 'NONE', #33354, #35988 ) ;
#3110=ORIENTED_EDGE ( 'NONE', *, *, #44313, .F. ) ;
#3121=VERTEX_POINT ( 'NONE', #19419 ) ;
#3193=SHAPE_REPRESENTATION_RELATIONSHIP ( 'NONE' , 'NONE' ,  #11272, #48464 ) ;
#3230=CARTESIAN_POINT ( 'NONE',  ( -45.55409385541306477, -14.20920654474410760, 70.91501325280044910 ) ) ;
#3246=CIRCLE ( 'NONE', #48063, 0.2400000000000006295 ) ;
#3258=DIRECTION ( 'NONE',  ( 1.224646799147353207E-16, 1.000000000000000000, -1.912410701131276611E-32 ) ) ;
#3392=EDGE_CURVE ( 'NONE', #47884, #9803, #13878, .T. ) ;
#3401=DIRECTION ( 'NONE',  ( 3.534154189880001717E-15, -4.519331686442879103E-31, -1.000000000000000000 ) ) ;
#3417=ORIENTED_EDGE ( 'NONE', *, *, #2315, .T. ) ;
#3483=DIRECTION ( 'NONE',  ( 1.224646799147353207E-16, 1.000000000000000000, -1.912410701131276611E-32 ) ) ;
#3489=AXIS2_PLACEMENT_3D ( 'NONE', #13287, #28581, #28341 ) ;
#3514=CARTESIAN_POINT ( 'NONE',  ( -46.47622156840087371, -14.20920654474410760, 70.13000000000000966 ) ) ;
#3525=AXIS2_PLACEMENT_3D ( 'NONE', #12335, #7692, #3989 ) ;
#3604=ORIENTED_EDGE ( 'NONE', *, *, #29594, .F. ) ;
#3661=CARTESIAN_POINT ( 'NONE',  ( -45.92409385541306222, -14.20920654474410760, 70.50000000000000000 ) ) ;
#3666=PLANE ( 'NONE',  #37356 ) ;
#3667=ORIENTED_EDGE ( 'NONE', *, *, #34327, .F. ) ;
#3683=( NAMED_UNIT ( * ) SI_UNIT ( $, .STERADIAN. ) SOLID_ANGLE_UNIT ( ) );
#3748=DIRECTION ( 'NONE',  ( 0.000000000000000000, 0.000000000000000000, 1.000000000000000000 ) ) ;
#3783=AXIS2_PLACEMENT_3D ( 'NONE', #10743, #30211, #48410 ) ;
#3891=ORIENTED_EDGE ( 'NONE', *, *, #10977, .T. ) ;
#3910=ORIENTED_EDGE ( 'NONE', *, *, #44313, .T. ) ;
#3960=DIRECTION ( 'NONE',  ( -5.551115123125782702E-17, -1.232595164407830946E-32, -1.000000000000000000 ) ) ;
#3989=DIRECTION ( 'NONE',  ( 0.000000000000000000, 1.000000000000000000, 0.000000000000000000 ) ) ;
#4001=CARTESIAN_POINT ( 'NONE',  ( -45.55409385541305767, -14.20920654474410760, 69.94787228701220272 ) ) ;
#4095=CARTESIAN_POINT ( 'NONE',  ( -46.47622156840087371, -14.20920654474410760, 70.13000000000000966 ) ) ;
#4106=PRODUCT_CONTEXT ( 'NONE', #18033, 'mechanical' ) ;
#4109=ADVANCED_FACE ( 'NONE', ( #30131 ), #41195, .F. ) ;
#4121=EDGE_CURVE ( 'NONE', #11700, #14807, #22242, .T. ) ;
#4147=ORIENTED_EDGE ( 'NONE', *, *, #32968, .T. ) ;
#4236=CARTESIAN_POINT ( 'NONE',  ( -45.92409385541306222, -14.38986189584960051, 70.50000000000000000 ) ) ;
#4246=EDGE_CURVE ( 'NONE', #39133, #47884, #5298, .T. ) ;
#4257=EDGE_LOOP ( 'NONE', ( #5905, #13126, #4709 ) ) ;
#4283=AXIS2_PLACEMENT_3D ( 'NONE', #19465, #26371, #12323 ) ;
#4360=CARTESIAN_POINT ( 'NONE',  ( -46.47622156840087371, -14.20920654474410760, 70.87000000000000455 ) ) ;
#4366=ORIENTED_EDGE ( 'NONE', *, *, #8954, .F. ) ;
#4368=EDGE_CURVE ( 'NONE', #28537, #34367, #35325, .T. ) ;
#4381=EDGE_LOOP ( 'NONE', ( #1761, #28551, #42276, #23994 ) ) ;
#4481=EDGE_LOOP ( 'NONE', ( #41779, #2990, #21238, #11186, #8309, #41469, #17486, #17323, #14298, #13479, #11383, #24725, #26743 ) ) ;
#4509=TOROIDAL_SURFACE ( 'NONE', #21031, 2.260000000000000675, 0.2399999999999998246 ) ;
#4512=FACE_OUTER_BOUND ( 'NONE', #4381, .T. ) ;
#4521=FACE_OUTER_BOUND ( 'NONE', #9662, .T. ) ;
#4549=ORIENTED_EDGE ( 'NONE', *, *, #24624, .F. ) ;
#4613=CIRCLE ( 'NONE', #43966, 0.5560000000000009379 ) ;
#4616=AXIS2_PLACEMENT_3D ( 'NONE', #19764, #35001, #31317 ) ;
#4709=ORIENTED_EDGE ( 'NONE', *, *, #29594, .T. ) ;
#4738=AXIS2_PLACEMENT_3D ( 'NONE', #7386, #22386, #18676 ) ;
#4908=B_SPLINE_CURVE_WITH_KNOTS ( 'NONE', 3,
 ( #45602, #41644, #42, #15027 ),
 .UNSPECIFIED., .F., .F.,
 ( 4, 4 ),
 ( 0.001041996463600835783, 0.002493317452643607161 ),
 .UNSPECIFIED. ) ;
#4946=CARTESIAN_POINT ( 'NONE',  ( -45.98959949296318683, -14.20920654474410760, 69.94787228701220272 ) ) ;
#4995=( BOUNDED_CURVE ( )  B_SPLINE_CURVE ( 3, ( #9081, #31956, #13707, #17415 ),
 .UNSPECIFIED., .F., .F. ) 
 B_SPLINE_CURVE_WITH_KNOTS ( ( 4, 4 ),
 ( 6.147240100468659207, 6.419130513890513257 ),
 .UNSPECIFIED. ) 
 CURVE ( )  GEOMETRIC_REPRESENTATION_ITEM ( )  RATIONAL_B_SPLINE_CURVE ( ( 1.000000000000000000, 0.9938491152766115722, 0.9938491152766115722, 1.000000000000000000 ) ) 
 REPRESENTATION_ITEM ( '' )  );
#5004=CARTESIAN_POINT ( 'NONE',  ( -45.92409385541306222, -14.20920654474410760, 70.50000000000000000 ) ) ;
#5022=CARTESIAN_POINT ( 'NONE',  ( -44.72480688026392670, -12.91120565595568870, 70.87000000000000455 ) ) ;
#5026=DIRECTION ( 'NONE',  ( 0.000000000000000000, 0.000000000000000000, 1.000000000000000000 ) ) ;
#5173=DIRECTION ( 'NONE',  ( -2.867370864192053918E-15, -0.4461977533475101065, 0.8949343913984056931 ) ) ;
#5231=PLANE ( 'NONE',  #28345 ) ;
#5234=ORIENTED_EDGE ( 'NONE', *, *, #44465, .T. ) ;
#5298=CIRCLE ( 'NONE', #29651, 0.6570903894995150374 ) ;
#5321=EDGE_CURVE ( 'NONE', #1571, #25382, #34961, .T. ) ;
#5466=AXIS2_PLACEMENT_3D ( 'NONE', #44499, #24811, #25525 ) ;
#5487=DIRECTION ( 'NONE',  ( 1.224646799147353207E-16, 1.000000000000000000, -1.912410701131276611E-32 ) ) ;
#5608=DIRECTION ( 'NONE',  ( 0.000000000000000000, 0.000000000000000000, 1.000000000000000000 ) ) ;
#5700=FACE_OUTER_BOUND ( 'NONE', #46447, .T. ) ;
#5803=ORIENTED_EDGE ( 'NONE', *, *, #48186, .T. ) ;
#5818=ADVANCED_FACE ( 'NONE', ( #48656 ), #29756, .F. ) ;
#5846=ORIENTED_EDGE ( 'NONE', *, *, #10170, .T. ) ;
#5885=PLANE ( 'NONE',  #40255 ) ;
#5892=SPHERICAL_SURFACE ( 'NONE', #12647, 4.000000000000000000 ) ;
#5901=ORIENTED_EDGE ( 'NONE', *, *, #12149, .T. ) ;
#5905=ORIENTED_EDGE ( 'NONE', *, *, #7303, .F. ) ;
#5937=( NAMED_UNIT ( * ) PLANE_ANGLE_UNIT ( ) SI_UNIT ( $, .RADIAN. ) );
#5958=DIRECTION ( 'NONE',  ( 0.000000000000000000, 0.000000000000000000, 1.000000000000000000 ) ) ;
#6033=EDGE_CURVE ( 'NONE', #35489, #22569, #22660, .T. ) ;
#6120=EDGE_CURVE ( 'NONE', #24736, #45017, #14734, .T. ) ;
#6229=CARTESIAN_POINT ( 'NONE',  ( -45.55409385541306477, -12.91120565595568692, 71.69928697514914973 ) ) ;
#6260=CARTESIAN_POINT ( 'NONE',  ( -45.92409385541306222, -14.20920654474410760, 70.50000000000000000 ) ) ;
#6287=ORIENTED_EDGE ( 'NONE', *, *, #9883, .F. ) ;
#6290=FACE_OUTER_BOUND ( 'NONE', #18932, .T. ) ;
#6339=EDGE_CURVE ( 'NONE', #41197, #3121, #8491, .T. ) ;
#6346=AXIS2_PLACEMENT_3D ( 'NONE', #22278, #30897, #30173 ) ;
#6375=AXIS2_PLACEMENT_3D ( 'NONE', #46465, #21077, #13659 ) ;
#6401=VECTOR ( 'NONE', #31165, 1000.000000000000000 ) ;
#6429=CARTESIAN_POINT ( 'NONE',  ( -45.50908060261262023, -14.20920654474410760, 70.13000000000000966 ) ) ;
#6476=LINE ( 'NONE', #13829, #35708 ) ;
#6483=CARTESIAN_POINT ( 'NONE',  ( -45.92409385541306222, -14.20920654474410760, 70.50000000000000000 ) ) ;
#6571=ORIENTED_EDGE ( 'NONE', *, *, #42142, .F. ) ;
#6580=FACE_BOUND ( 'NONE', #38055, .T. ) ;
#6622=AXIS2_PLACEMENT_3D ( 'NONE', #14535, #14063, #21497 ) ;
#6664=DIRECTION ( 'NONE',  ( 0.000000000000000000, 0.000000000000000000, 1.000000000000000000 ) ) ;
#6700=DIRECTION ( 'NONE',  ( 1.000000000000000000, -1.224646799147353207E-16, 6.695352868347749370E-17 ) ) ;
#6971=AXIS2_PLACEMENT_3D ( 'NONE', #45237, #45473, #26023 ) ;
#6981=ORIENTED_EDGE ( 'NONE', *, *, #6033, .T. ) ;
#7011=EDGE_CURVE ( 'NONE', #22569, #35836, #11691, .T. ) ;
#7068=VERTEX_POINT ( 'NONE', #11652 ) ;
#7120=DIRECTION ( 'NONE',  ( -3.159776991290051445E-16, -1.000000000000000000, -6.457808579236824910E-31 ) ) ;
#7133=FACE_OUTER_BOUND ( 'NONE', #32474, .T. ) ;
#7134=VERTEX_POINT ( 'NONE', #46118 ) ;
#7250=CARTESIAN_POINT ( 'NONE',  ( -46.29409385541305966, -12.70920654474410760, 71.79999999999999716 ) ) ;
#7303=EDGE_CURVE ( 'NONE', #18791, #7630, #2304, .T. ) ;
#7311=VERTEX_POINT ( 'NONE', #18476 ) ;
#7353=CIRCLE ( 'NONE', #40337, 0.2400000000000006295 ) ;
#7386=CARTESIAN_POINT ( 'NONE',  ( -46.29409385541305966, -14.20920654474410760, 71.05212771298751306 ) ) ;
#7457=AXIS2_PLACEMENT_3D ( 'NONE', #26026, #18370, #42448 ) ;
#7514=EDGE_CURVE ( 'NONE', #48327, #40177, #17985, .T. ) ;
#7538=ORIENTED_EDGE ( 'NONE', *, *, #29440, .F. ) ;
#7564=DIRECTION ( 'NONE',  ( 1.224646799147353207E-16, 1.000000000000000000, -1.912410701131276611E-32 ) ) ;
#7566=ORIENTED_EDGE ( 'NONE', *, *, #42142, .T. ) ;
#7583=DIRECTION ( 'NONE',  ( -3.485387654165294196E-16, 2.355958133329952458E-32, -1.000000000000000000 ) ) ;
#7584=EDGE_CURVE ( 'NONE', #10113, #38529, #28503, .T. ) ;
#7604=EDGE_CURVE ( 'NONE', #28537, #12407, #20371, .T. ) ;
#7630=VERTEX_POINT ( 'NONE', #36578 ) ;
#7678=ORIENTED_EDGE ( 'NONE', *, *, #1289, .T. ) ;
#7692=DIRECTION ( 'NONE',  ( 4.267285103686815209E-17, -5.292884291094200710E-16, -1.000000000000000000 ) ) ;
#7713=DIRECTION ( 'NONE',  ( 0.4461977533473618363, -0.8949343913984794119, -2.476895096511286888E-17 ) ) ;
#7729=EDGE_CURVE ( 'NONE', #37849, #7068, #26986, .T. ) ;
#7733=ORIENTED_EDGE ( 'NONE', *, *, #10699, .T. ) ;
#7800=AXIS2_PLACEMENT_3D ( 'NONE', #37699, #14302, #48297 ) ;
#7809=ORIENTED_EDGE ( 'NONE', *, *, #35557, .F. ) ;
#7811=VECTOR ( 'NONE', #32667, 1000.000000000000000 ) ;
#7814=LINE ( 'NONE', #29963, #38453 ) ;
#7819=EDGE_LOOP ( 'NONE', ( #46777, #19152, #4147, #26110, #7538 ) ) ;
#7885=ORIENTED_EDGE ( 'NONE', *, *, #44578, .F. ) ;
#7887=FACE_OUTER_BOUND ( 'NONE', #44704, .T. ) ;
#7931=PLANE ( 'NONE',  #18487 ) ;
#8069=DIRECTION ( 'NONE',  ( -4.267285103686820140E-17, 1.935130192142698484E-16, 1.000000000000000000 ) ) ;
#8094=VERTEX_POINT ( 'NONE', #40723 ) ;
#8301=DIRECTION ( 'NONE',  ( 3.534154189880001717E-15, -4.519331686442879103E-31, -1.000000000000000000 ) ) ;
#8309=ORIENTED_EDGE ( 'NONE', *, *, #3392, .F. ) ;
#8325=ORIENTED_EDGE ( 'NONE', *, *, #42461, .F. ) ;
#8452=CARTESIAN_POINT ( 'NONE',  ( -45.92409385541306222, -14.20920654474410760, 70.50000000000000000 ) ) ;
#8486=CIRCLE ( 'NONE', #12415, 0.5560000000000009379 ) ;
#8491=CIRCLE ( 'NONE', #42313, 0.5560000000000009379 ) ;
#8602=CIRCLE ( 'NONE', #48692, 0.5560000000000009379 ) ;
#8635=DIRECTION ( 'NONE',  ( 1.224646799147353207E-16, 1.000000000000000000, -1.912410701131276611E-32 ) ) ;
#8747=ADVANCED_FACE ( 'NONE', ( #14709 ), #41100, .F. ) ;
#8789=VECTOR ( 'NONE', #7713, 1000.000000000000227 ) ;
#8819=ADVANCED_FACE ( 'NONE', ( #1184 ), #43264, .F. ) ;
#8838=ORIENTED_EDGE ( 'NONE', *, *, #35557, .T. ) ;
#8936=ORIENTED_EDGE ( 'NONE', *, *, #6120, .F. ) ;
#8954=EDGE_CURVE ( 'NONE', #39770, #41197, #4995, .T. ) ;
#8964=DIRECTION ( 'NONE',  ( 1.224646799147353207E-16, 1.000000000000000000, -1.912410701131276611E-32 ) ) ;
#8980=SPHERICAL_SURFACE ( 'NONE', #45766, 4.000000000000000000 ) ;
#9074=CARTESIAN_POINT ( 'NONE',  ( -46.38423044223897307, -13.72754205882879042, 70.87000000000000455 ) ) ;
#9081=CARTESIAN_POINT ( 'NONE',  ( -46.47622156840087371, -14.20920654474410760, 70.43449436244988249 ) ) ;
#9090=DIRECTION ( 'NONE',  ( 0.000000000000000000, 0.000000000000000000, 1.000000000000000000 ) ) ;
#9152=EDGE_LOOP ( 'NONE', ( #18782, #10145, #7566, #32624 ) ) ;
#9214=ORIENTED_EDGE ( 'NONE', *, *, #38728, .T. ) ;
#9230=AXIS2_PLACEMENT_3D ( 'NONE', #9981, #47418, #47170 ) ;
#9251=CARTESIAN_POINT ( 'NONE',  ( -45.92409385541306222, -13.51240245935757578, 70.50000000000000000 ) ) ;
#9258=ORIENTED_EDGE ( 'NONE', *, *, #48395, .T. ) ;
#9381=VECTOR ( 'NONE', #38543, 1000.000000000000114 ) ;
#9511=ORIENTED_EDGE ( 'NONE', *, *, #11919, .T. ) ;
#9556=DIRECTION ( 'NONE',  ( 0.000000000000000000, 1.000000000000000000, 0.000000000000000000 ) ) ;
#9564=ADVANCED_FACE ( 'NONE', ( #22608 ), #11288, .T. ) ;
#9602=CARTESIAN_POINT ( 'NONE',  ( -45.37196614242555626, -14.20920654474410760, 70.87000000000000455 ) ) ;
#9649=PRODUCT_DEFINITION ( 'UNKNOWN', '', #17973, #19903 ) ;
#9662=EDGE_LOOP ( 'NONE', ( #27975, #44447, #233 ) ) ;
#9695=CARTESIAN_POINT ( 'NONE',  ( -46.29409385541305966, -16.70920654474410938, 70.50000000000000000 ) ) ;
#9719=ORIENTED_EDGE ( 'NONE', *, *, #20772, .F. ) ;
#9790=DIRECTION ( 'NONE',  ( 2.342027643795563533E-48, 1.912410701131276611E-32, 1.000000000000000000 ) ) ;
#9803=VERTEX_POINT ( 'NONE', #26039 ) ;
#9833=CIRCLE ( 'NONE', #3525, 3.982850737850967437 ) ;
#9883=EDGE_CURVE ( 'NONE', #30449, #7311, #38562, .T. ) ;
#9935=ORIENTED_EDGE ( 'NONE', *, *, #37779, .T. ) ;
#9936=AXIS2_PLACEMENT_3D ( 'NONE', #38398, #23657, #754 ) ;
#9981=CARTESIAN_POINT ( 'NONE',  ( -45.92409385541306222, -14.20920654474410760, 70.50000000000000000 ) ) ;
#10038=EDGE_LOOP ( 'NONE', ( #48294, #12256, #12435, #341 ) ) ;
#10054=DIRECTION ( 'NONE',  ( 0.4461977533473618363, -0.8949343913984794119, -2.476895096511287196E-17 ) ) ;
#10097=ORIENTED_EDGE ( 'NONE', *, *, #2640, .T. ) ;
#10113=VERTEX_POINT ( 'NONE', #47897 ) ;
#10122=ORIENTED_EDGE ( 'NONE', *, *, #47583, .F. ) ;
#10124=VECTOR ( 'NONE', #13330, 1000.000000000000000 ) ;
#10145=ORIENTED_EDGE ( 'NONE', *, *, #25506, .T. ) ;
#10152=EDGE_CURVE ( 'NONE', #44898, #30449, #46424, .T. ) ;
#10170=EDGE_CURVE ( 'NONE', #11860, #14807, #18565, .T. ) ;
#10224=DIRECTION ( 'NONE',  ( 0.000000000000000000, 0.000000000000000000, 1.000000000000000000 ) ) ;
#10243=CONICAL_SURFACE ( 'NONE', #1581, 0.5560000000000009379, 0.06981317007976595157 ) ;
#10249=VERTEX_POINT ( 'NONE', #43187 ) ;
#10261=DIRECTION ( 'NONE',  ( 1.224646799147353207E-16, 1.000000000000000000, -1.912410701131276611E-32 ) ) ;
#10356=EDGE_CURVE ( 'NONE', #39133, #30449, #34540, .T. ) ;
#10359=EDGE_CURVE ( 'NONE', #34367, #31776, #1524, .T. ) ;
#10448=CARTESIAN_POINT ( 'NONE',  ( -45.55409385541305767, -14.20920654474410760, 69.94787228701220272 ) ) ;
#10598=DIRECTION ( 'NONE',  ( 1.224646799147353207E-16, 1.000000000000000000, -1.912410701131276611E-32 ) ) ;
#10622=DIRECTION ( 'NONE',  ( 0.000000000000000000, 0.000000000000000000, 1.000000000000000000 ) ) ;
#10628=CARTESIAN_POINT ( 'NONE',  ( -46.29409385541305966, -12.76354662275040219, 71.04301729251712061 ) ) ;
#10664=CIRCLE ( 'NONE', #26413, 0.5560000000000009379 ) ;
#10699=EDGE_CURVE ( 'NONE', #37913, #14807, #25319, .T. ) ;
#10734=CARTESIAN_POINT ( 'NONE',  ( -45.92409385541306222, -14.38986189584960051, 70.50000000000000000 ) ) ;
#10743=CARTESIAN_POINT ( 'NONE',  ( -45.92409385541306222, -14.20920654474410760, 70.50000000000000000 ) ) ;
#10908=AXIS2_PLACEMENT_3D ( 'NONE', #42449, #46630, #30647 ) ;
#10920=ORIENTED_EDGE ( 'NONE', *, *, #27935, .T. ) ;
#10959=ORIENTED_EDGE ( 'NONE', *, *, #7604, .F. ) ;
#10977=EDGE_CURVE ( 'NONE', #39895, #38529, #36245, .T. ) ;
#10995=AXIS2_PLACEMENT_3D ( 'NONE', #25108, #32947, #21887 ) ;
#10999=CARTESIAN_POINT ( 'NONE',  ( -44.62409385541305795, -12.70920654474410760, 70.87000000000000455 ) ) ;
#11011=CARTESIAN_POINT ( 'NONE',  ( -45.92409385541306222, -14.90920654474410867, 70.50000000000000000 ) ) ;
#11042=LINE ( 'NONE', #11291, #22837 ) ;
#11076=CIRCLE ( 'NONE', #40175, 3.982850737850970990 ) ;
#11093=EDGE_CURVE ( 'NONE', #11700, #7134, #40199, .T. ) ;
#11151=VECTOR ( 'NONE', #2896, 1000.000000000000000 ) ;
#11164=DIRECTION ( 'NONE',  ( -1.642720032068235908E-15, -0.8949343913984794119, 0.4461977533473619473 ) ) ;
#11177=DIRECTION ( 'NONE',  ( 1.164780374791175599E-15, -0.8949343913984055821, -0.4461977533475099955 ) ) ;
#11186=ORIENTED_EDGE ( 'NONE', *, *, #22491, .T. ) ;
#11194=DIRECTION ( 'NONE',  ( 1.224646799147353207E-16, 1.000000000000000000, -1.912410701131276611E-32 ) ) ;
#11218=CARTESIAN_POINT ( 'NONE',  ( -45.92409385541306222, -13.70421070448077039, 68.00000000000000000 ) ) ;
#11272=SHAPE_REPRESENTATION ( 'Attachment Screw', ( #29031 ), #23534 ) ;
#11288=PLANE ( 'NONE',  #37724 ) ;
#11291=CARTESIAN_POINT ( 'NONE',  ( -46.29409385541305966, -14.20920654474410760, 71.05212771298751306 ) ) ;
#11296=CARTESIAN_POINT ( 'NONE',  ( -45.85858821786293049, -14.20920654474410760, 69.94787228701220272 ) ) ;
#11340=EDGE_LOOP ( 'NONE', ( #7885, #37907, #927, #6981, #29060, #37389, #38132, #9719, #16973, #38195, #36495, #34333, #14893 ) ) ;
#11343=DIRECTION ( 'NONE',  ( 0.000000000000000000, 0.000000000000000000, 1.000000000000000000 ) ) ;
#11369=DIRECTION ( 'NONE',  ( 9.063790940987422061E-17, 0.3090169943749398462, 0.9510565162951560847 ) ) ;
#11374=CARTESIAN_POINT ( 'NONE',  ( -45.92409385541306222, -13.70421070448076861, 70.50000000000000000 ) ) ;
#11383=ORIENTED_EDGE ( 'NONE', *, *, #28446, .F. ) ;
#11425=DIRECTION ( 'NONE',  ( -5.551115123125782702E-17, -1.232595164407830946E-32, -1.000000000000000000 ) ) ;
#11467=CARTESIAN_POINT ( 'NONE',  ( -46.48018488037470064, -16.43194983366065642, 70.50000000000000000 ) ) ;
#11533=EDGE_CURVE ( 'NONE', #9803, #22122, #26411, .T. ) ;
#11652=CARTESIAN_POINT ( 'NONE',  ( -45.55409385541306477, -14.20920654474410760, 71.05212771298751306 ) ) ;
#11658=FACE_OUTER_BOUND ( 'NONE', #38400, .T. ) ;
#11679=AXIS2_PLACEMENT_3D ( 'NONE', #34598, #15634, #26745 ) ;
#11691=CIRCLE ( 'NONE', #28976, 3.951441697420869481 ) ;
#11699=EDGE_CURVE ( 'NONE', #35489, #41576, #26847, .T. ) ;
#11700=VERTEX_POINT ( 'NONE', #6429 ) ;
#11802=DIRECTION ( 'NONE',  ( 1.224646799147353207E-16, 1.000000000000000000, -1.912410701131276611E-32 ) ) ;
#11810=DIRECTION ( 'NONE',  ( 1.224646799147353207E-16, 1.000000000000000000, -1.912410701131276611E-32 ) ) ;
#11835=DIRECTION ( 'NONE',  ( 1.224646799147353207E-16, 1.000000000000000000, -1.912410701131276611E-32 ) ) ;
#11853=CARTESIAN_POINT ( 'NONE',  ( -45.92409385541306222, -17.80920654474411435, 69.25000000000000000 ) ) ;
#11860=VERTEX_POINT ( 'NONE', #18960 ) ;
#11871=AXIS2_PLACEMENT_3D ( 'NONE', #43987, #36784, #29924 ) ;
#11889=ORIENTED_EDGE ( 'NONE', *, *, #4368, .T. ) ;
#11919=EDGE_CURVE ( 'NONE', #32734, #41576, #3246, .T. ) ;
#11979=VERTEX_POINT ( 'NONE', #1207 ) ;
#11980=CARTESIAN_POINT ( 'NONE',  ( -46.47622156840087371, -14.20920654474410760, 70.13000000000000966 ) ) ;
#12133=ORIENTED_EDGE ( 'NONE', *, *, #20178, .F. ) ;
#12149=EDGE_CURVE ( 'NONE', #10113, #17364, #18203, .T. ) ;
#12165=ORIENTED_EDGE ( 'NONE', *, *, #10699, .F. ) ;
#12256=ORIENTED_EDGE ( 'NONE', *, *, #25987, .T. ) ;
#12257=ADVANCED_FACE ( 'NONE', ( #24960 ), #8980, .T. ) ;
#12287=EDGE_CURVE ( 'NONE', #1571, #37218, #30829, .T. ) ;
#12291=ORIENTED_EDGE ( 'NONE', *, *, #45086, .F. ) ;
#12323=DIRECTION ( 'NONE',  ( -3.484385612528001215E-15, 0.000000000000000000, 1.000000000000000000 ) ) ;
#12335=CARTESIAN_POINT ( 'NONE',  ( -45.92409385541306932, -16.70920654474410938, 70.87000000000000455 ) ) ;
#12365=DIRECTION ( 'NONE',  ( 1.224646799147353207E-16, 1.000000000000000000, -1.912410701131276611E-32 ) ) ;
#12379=CONICAL_SURFACE ( 'NONE', #26549, 3077.683537175336824, 1.256637061435925240 ) ;
#12407=VERTEX_POINT ( 'NONE', #40453 ) ;
#12415=AXIS2_PLACEMENT_3D ( 'NONE', #47444, #13677, #5608 ) ;
#12422=LINE ( 'NONE', #12900, #14663 ) ;
#12435=ORIENTED_EDGE ( 'NONE', *, *, #28012, .T. ) ;
#12438=CARTESIAN_POINT ( 'NONE',  ( -45.92409385541306222, -14.20017296387473316, 71.05663168951063824 ) ) ;
#12445=DIRECTION ( 'NONE',  ( 0.000000000000000000, 0.000000000000000000, 1.000000000000000000 ) ) ;
#12498=FACE_OUTER_BOUND ( 'NONE', #32877, .T. ) ;
#12523=FACE_OUTER_BOUND ( 'NONE', #7819, .T. ) ;
#12552=DIRECTION ( 'NONE',  ( 0.000000000000000000, -0.8949343913984053600, -0.4461977533475104396 ) ) ;
#12567=ORIENTED_EDGE ( 'NONE', *, *, #28012, .F. ) ;
#12594=ORIENTED_EDGE ( 'NONE', *, *, #47060, .T. ) ;
#12628=DIRECTION ( 'NONE',  ( -1.224646799147353207E-16, -1.000000000000000000, 1.912410701131276611E-32 ) ) ;
#12630=DIRECTION ( 'NONE',  ( 1.000000000000000000, -1.224646799147353207E-16, 3.142942573426604379E-15 ) ) ;
#12647=AXIS2_PLACEMENT_3D ( 'NONE', #21810, #18344, #39379 ) ;
#12660=DIRECTION ( 'NONE',  ( 1.224646799147353207E-16, 1.000000000000000000, -1.912410701131276611E-32 ) ) ;
#12724=DIRECTION ( 'NONE',  ( 1.015202570477164967E-16, 0.3090169943749398462, -0.9510565162951560847 ) ) ;
#12845=DIRECTION ( 'NONE',  ( -2.112005902016726815E-14, 0.000000000000000000, -1.000000000000000000 ) ) ;
#12850=CARTESIAN_POINT ( 'NONE',  ( -46.47622156840087371, -14.20920654474410760, 70.13000000000000966 ) ) ;
#12889=CARTESIAN_POINT ( 'NONE',  ( -46.29409385541305255, -13.72754205882879042, 70.03986341317408915 ) ) ;
#12900=CARTESIAN_POINT ( 'NONE',  ( -46.29409385541305966, -14.20920654474410760, 71.05212771298751306 ) ) ;
#13068=VECTOR ( 'NONE', #12724, 1000.000000000000114 ) ;
#13108=DIRECTION ( 'NONE',  ( 1.224646799147353207E-16, 1.000000000000000000, -1.912410701131276611E-32 ) ) ;
#13125=CARTESIAN_POINT ( 'NONE',  ( -45.92409385541306222, -13.70421070448076861, 72.76000000000000512 ) ) ;
#13126=ORIENTED_EDGE ( 'NONE', *, *, #18776, .F. ) ;
#13141=AXIS2_PLACEMENT_3D ( 'NONE', #33288, #15311, #11164 ) ;
#13191=AXIS2_PLACEMENT_3D ( 'NONE', #34954, #8635, #28317 ) ;
#13238=AXIS2_PLACEMENT_3D ( 'NONE', #33486, #48527, #18734 ) ;
#13256=EDGE_LOOP ( 'NONE', ( #22517, #30822, #31250, #14396 ) ) ;
#13287=CARTESIAN_POINT ( 'NONE',  ( -45.92409385541306222, -13.70421070448077039, 70.50000000000000000 ) ) ;
#13290=CARTESIAN_POINT ( 'NONE',  ( -45.37196614242555626, -14.20920654474410760, 70.87000000000000455 ) ) ;
#13298=FILL_AREA_STYLE_COLOUR ( '', #33109 ) ;
#13326=CARTESIAN_POINT ( 'NONE',  ( -45.55409385541306477, -13.72754205882879042, 70.96013658682592506 ) ) ;
#13330=DIRECTION ( 'NONE',  ( 1.224646799147353207E-16, 1.000000000000000000, -1.912410701131276611E-32 ) ) ;
#13383=DIRECTION ( 'NONE',  ( 1.224646799147353207E-16, 1.000000000000000000, -1.912410701131276611E-32 ) ) ;
#13426=VECTOR ( 'NONE', #7583, 1000.000000000000000 ) ;
#13453=CARTESIAN_POINT ( 'NONE',  ( -46.29409385541305966, -12.91120565595568692, 71.69928697514914973 ) ) ;
#13479=ORIENTED_EDGE ( 'NONE', *, *, #21839, .F. ) ;
#13485=TOROIDAL_SURFACE ( 'NONE', #41810, 2.260000000000000675, 0.2399999999999998246 ) ;
#13494=DIRECTION ( 'NONE',  ( 4.267285103686815209E-17, -5.292884291094200710E-16, -1.000000000000000000 ) ) ;
#13566=CARTESIAN_POINT ( 'NONE',  ( -45.55409385541306477, -13.24559821555319239, 71.00222776205102093 ) ) ;
#13592=CARTESIAN_POINT ( 'NONE',  ( -45.37196614242555626, -14.20920654474410760, 70.43449436244726769 ) ) ;
#13593=DIRECTION ( 'NONE',  ( 0.000000000000000000, 0.000000000000000000, 1.000000000000000000 ) ) ;
#13659=DIRECTION ( 'NONE',  ( 0.000000000000000000, 0.000000000000000000, 1.000000000000000000 ) ) ;
#13677=DIRECTION ( 'NONE',  ( 1.224646799147353207E-16, 1.000000000000000000, -1.912410701131276611E-32 ) ) ;
#13694=DIRECTION ( 'NONE',  ( 1.224646799147353207E-16, 1.000000000000000000, -1.912410701131276611E-32 ) ) ;
#13707=CARTESIAN_POINT ( 'NONE',  ( -46.48223616206310993, -14.19714313411900619, 70.52197034960447297 ) ) ;
#13751=CYLINDRICAL_SURFACE ( 'NONE', #10995, 2.500000000000002220 ) ;
#13761=B_SPLINE_CURVE_WITH_KNOTS ( 'NONE', 3,
 ( #32787, #21714, #22206, #33016 ),
 .UNSPECIFIED., .F., .F.,
 ( 4, 4 ),
 ( 0.001310108020964423923, 0.002761379516307285557 ),
 .UNSPECIFIED. ) ;
#13781=ADVANCED_FACE ( 'NONE', ( #47892 ), #2149, .F. ) ;
#13829=CARTESIAN_POINT ( 'NONE',  ( -46.47622156840087371, -14.20920654474410760, 70.13000000000000966 ) ) ;
#13878=CIRCLE ( 'NONE', #28831, 3.982850737850967437 ) ;
#13909=ORIENTED_EDGE ( 'NONE', *, *, #4121, .T. ) ;
#13997=AXIS2_PLACEMENT_3D ( 'NONE', #17419, #14183, #40547 ) ;
#14005=ADVANCED_FACE ( 'NONE', ( #45129 ), #4509, .T. ) ;
#14032=AXIS2_PLACEMENT_3D ( 'NONE', #8452, #23734, #19289 ) ;
#14063=DIRECTION ( 'NONE',  ( -1.000000000000000000, 3.159776991290051445E-16, -3.534154189880001717E-15 ) ) ;
#14079=ADVANCED_FACE ( 'NONE', ( #5700 ), #20213, .F. ) ;
#14113=CARTESIAN_POINT ( 'NONE',  ( -45.92409385541306222, -14.20920654474410760, 70.50000000000000000 ) ) ;
#14183=DIRECTION ( 'NONE',  ( 1.224646799147353207E-16, 1.000000000000000000, -1.912410701131276611E-32 ) ) ;
#14252=AXIS2_PLACEMENT_3D ( 'NONE', #37787, #31132, #19320 ) ;
#14288=CARTESIAN_POINT ( 'NONE',  ( -46.29409385541305966, -14.20920654474410760, 70.91501325280044910 ) ) ;
#14298=ORIENTED_EDGE ( 'NONE', *, *, #31234, .F. ) ;
#14302=DIRECTION ( 'NONE',  ( 1.224646799147353207E-16, 1.000000000000000000, -1.912410701131276611E-32 ) ) ;
#14396=ORIENTED_EDGE ( 'NONE', *, *, #29317, .T. ) ;
#14398=ORIENTED_EDGE ( 'NONE', *, *, #7729, .T. ) ;
#14481=( LENGTH_UNIT ( ) NAMED_UNIT ( * ) SI_UNIT ( .MILLI., .METRE. ) );
#14535=CARTESIAN_POINT ( 'NONE',  ( -45.55409385541306477, -14.20920654474410760, 71.05212771298751306 ) ) ;
#14553=CARTESIAN_POINT ( 'NONE',  ( -45.92409385541306222, -13.51240245935757578, 68.09574468085106957 ) ) ;
#14556=CIRCLE ( 'NONE', #24040, 0.5560000000000009379 ) ;
#14597=VERTEX_POINT ( 'NONE', #4360 ) ;
#14613=B_SPLINE_CURVE_WITH_KNOTS ( 'NONE', 3,
 ( #31949, #39338, #9074, #31225 ),
 .UNSPECIFIED., .F., .F.,
 ( 4, 4 ),
 ( 0.001041996463600832314, 0.002493317452643608895 ),
 .UNSPECIFIED. ) ;
#14663=VECTOR ( 'NONE', #1097, 1000.000000000000000 ) ;
#14709=FACE_OUTER_BOUND ( 'NONE', #37777, .T. ) ;
#14734=CIRCLE ( 'NONE', #17916, 1.350000000000004086 ) ;
#14739=ADVANCED_FACE ( 'NONE', ( #43664 ), #12379, .F. ) ;
#14767=DIRECTION ( 'NONE',  ( 1.224646799147353207E-16, 1.000000000000000000, -1.912410701131276611E-32 ) ) ;
#14807=VERTEX_POINT ( 'NONE', #39866 ) ;
#14823=CARTESIAN_POINT ( 'NONE',  ( -46.48018488037470064, -16.43194983366065642, 70.50000000000000000 ) ) ;
#14838=CARTESIAN_POINT ( 'NONE',  ( -45.37196614242555626, -14.20920654474410760, 70.43449436244726769 ) ) ;
#14868=PLANE ( 'NONE',  #1658 ) ;
#14893=ORIENTED_EDGE ( 'NONE', *, *, #15928, .T. ) ;
#14918=VECTOR ( 'NONE', #18044, 1000.000000000000000 ) ;
#14975=CARTESIAN_POINT ( 'NONE',  ( -45.55409385541305767, -14.20920654474410760, 69.94787228701220272 ) ) ;
#15027=CARTESIAN_POINT ( 'NONE',  ( -45.50908060261262023, -14.20920654474410760, 70.13000000000000966 ) ) ;
#15051=CARTESIAN_POINT ( 'NONE',  ( -45.92409385541306222, -14.20920654474410760, 70.50000000000000000 ) ) ;
#15291=CARTESIAN_POINT ( 'NONE',  ( -47.13112723832431783, -12.89566876303303466, 70.50000000000000000 ) ) ;
#15311=DIRECTION ( 'NONE',  ( 3.020324423671394282E-15, -0.4461977533473619473, -0.8949343913984794119 ) ) ;
#15495=FACE_OUTER_BOUND ( 'NONE', #18830, .T. ) ;
#15584=CARTESIAN_POINT ( 'NONE',  ( -45.50908060261262023, -14.20920654474410760, 70.87000000000000455 ) ) ;
#15598=AXIS2_PLACEMENT_3D ( 'NONE', #11011, #42024, #23311 ) ;
#15634=DIRECTION ( 'NONE',  ( 1.224646799147353207E-16, 1.000000000000000000, -1.912410701131276611E-32 ) ) ;
#15659=ADVANCED_FACE ( 'NONE', ( #11658 ), #20020, .F. ) ;
#15683=DIRECTION ( 'NONE',  ( 1.224646799147353207E-16, 1.000000000000000000, -1.912410701131276611E-32 ) ) ;
#15744=VECTOR ( 'NONE', #131, 1000.000000000000227 ) ;
#15768=ORIENTED_EDGE ( 'NONE', *, *, #7729, .F. ) ;
#15806=CARTESIAN_POINT ( 'NONE',  ( -46.29409385541305255, -12.91120565595569758, 69.30071302485083606 ) ) ;
#15852=ORIENTED_EDGE ( 'NONE', *, *, #48186, .F. ) ;
#15868=ORIENTED_EDGE ( 'NONE', *, *, #32968, .F. ) ;
#15883=CARTESIAN_POINT ( 'NONE',  ( -45.92409385541306932, -16.70920654474410938, 70.13000000000000966 ) ) ;
#15928=EDGE_CURVE ( 'NONE', #48327, #38900, #28207, .T. ) ;
#15976=DIRECTION ( 'NONE',  ( 1.000000000000000000, -1.224646799147353207E-16, 6.695352868347749370E-17 ) ) ;
#15985=ORIENTED_EDGE ( 'NONE', *, *, #42754, .T. ) ;
#15995=AXIS2_PLACEMENT_3D ( 'NONE', #5004, #5487, #5958 ) ;
#16049=DIRECTION ( 'NONE',  ( -5.551115123125782702E-17, -1.232595164407830946E-32, -1.000000000000000000 ) ) ;
#16065=ORIENTED_EDGE ( 'NONE', *, *, #32650, .F. ) ;
#16076=FACE_OUTER_BOUND ( 'NONE', #4257, .T. ) ;
#16143=ADVANCED_FACE ( 'NONE', ( #6580, #36582 ), #40786, .F. ) ;
#16175=CARTESIAN_POINT ( 'NONE',  ( -46.29409385541305255, -12.76354662275040219, 69.95698270748289360 ) ) ;
#16282=ORIENTED_EDGE ( 'NONE', *, *, #46524, .T. ) ;
#16339=DIRECTION ( 'NONE',  ( 0.000000000000000000, -1.912410701131276611E-32, -1.000000000000000000 ) ) ;
#16407=VERTEX_POINT ( 'NONE', #2340 ) ;
#16430=CARTESIAN_POINT ( 'NONE',  ( -45.92409385541306932, -16.70920654474410938, 70.87000000000000455 ) ) ;
#16460=DIRECTION ( 'NONE',  ( 1.224646799147353207E-16, 1.000000000000000000, -1.912410701131276611E-32 ) ) ;
#16488=AXIS2_PLACEMENT_3D ( 'NONE', #34681, #11802, #45301 ) ;
#16578=EDGE_LOOP ( 'NONE', ( #22325, #47911, #13909, #46855 ) ) ;
#16597=CARTESIAN_POINT ( 'NONE',  ( -46.33910710821349710, -14.20920654474410760, 70.13000000000000966 ) ) ;
#16601=ORIENTED_EDGE ( 'NONE', *, *, #20772, .T. ) ;
#16642=ADVANCED_FACE ( 'NONE', ( #4521 ), #30886, .F. ) ;
#16669=EDGE_CURVE ( 'NONE', #18791, #37218, #33120, .T. ) ;
#16681=EDGE_LOOP ( 'NONE', ( #27054, #24149, #21646, #3667 ) ) ;
#16774=VERTEX_POINT ( 'NONE', #32560 ) ;
#16830=ORIENTED_EDGE ( 'NONE', *, *, #5321, .T. ) ;
#16833=CIRCLE ( 'NONE', #48302, 0.5560000000000009379 ) ;
#16837=VERTEX_POINT ( 'NONE', #2998 ) ;
#16857=CARTESIAN_POINT ( 'NONE',  ( -45.92409385541306222, -14.20920654474410760, 70.50000000000000000 ) ) ;
#16873=ADVANCED_FACE ( 'NONE', ( #40915 ), #47119, .F. ) ;
#16891=DIRECTION ( 'NONE',  ( 0.000000000000000000, 0.000000000000000000, 1.000000000000000000 ) ) ;
#16973=ORIENTED_EDGE ( 'NONE', *, *, #27684, .T. ) ;
#16980=ORIENTED_EDGE ( 'NONE', *, *, #7584, .F. ) ;
#16994=ORIENTED_EDGE ( 'NONE', *, *, #1289, .F. ) ;
#17110=ORIENTED_EDGE ( 'NONE', *, *, #27684, .F. ) ;
#17176=CIRCLE ( 'NONE', #13997, 0.5560000000000009379 ) ;
#17181=CARTESIAN_POINT ( 'NONE',  ( -46.47622156840087371, -14.20920654474410760, 70.87000000000000455 ) ) ;
#17243=EDGE_CURVE ( 'NONE', #44898, #7311, #48306, .T. ) ;
#17283=VECTOR ( 'NONE', #20129, 1000.000000000000000 ) ;
#17289=AXIS2_PLACEMENT_3D ( 'NONE', #2317, #28184, #24973 ) ;
#17323=ORIENTED_EDGE ( 'NONE', *, *, #32650, .T. ) ;
#17361=CIRCLE ( 'NONE', #33055, 3.982850737850970990 ) ;
#17364=VERTEX_POINT ( 'NONE', #11853 ) ;
#17378=EDGE_CURVE ( 'NONE', #11979, #11700, #4908, .T. ) ;
#17415=CARTESIAN_POINT ( 'NONE',  ( -46.47622156840087371, -14.20920654474410760, 70.56550563755013172 ) ) ;
#17419=CARTESIAN_POINT ( 'NONE',  ( -45.92409385541306222, -14.20920654474410760, 70.50000000000000000 ) ) ;
#17427=CIRCLE ( 'NONE', #23752, 3.951441697420975618 ) ;
#17463=FACE_OUTER_BOUND ( 'NONE', #9152, .T. ) ;
#17486=ORIENTED_EDGE ( 'NONE', *, *, #35171, .F. ) ;
#17491=ORIENTED_EDGE ( 'NONE', *, *, #34327, .T. ) ;
#17573=ORIENTED_EDGE ( 'NONE', *, *, #29317, .F. ) ;
#17595=DIRECTION ( 'NONE',  ( 1.224646799147353207E-16, 1.000000000000000000, -1.912410701131276611E-32 ) ) ;
#17648=CIRCLE ( 'NONE', #45203, 0.5560000000000009379 ) ;
#17667=CARTESIAN_POINT ( 'NONE',  ( -45.55409385541305767, -16.70920654474410938, 70.50000000000000000 ) ) ;
#17873=FACE_OUTER_BOUND ( 'NONE', #16578, .T. ) ;
#17916=AXIS2_PLACEMENT_3D ( 'NONE', #34235, #14767, #38170 ) ;
#17925=CARTESIAN_POINT ( 'NONE',  ( -45.92409385541306222, -14.80920654474410902, 69.15000000000000568 ) ) ;
#17937=ORIENTED_EDGE ( 'NONE', *, *, #45803, .T. ) ;
#17972=EDGE_CURVE ( 'NONE', #7134, #19297, #37717, .T. ) ;
#17973=PRODUCT_DEFINITION_FORMATION_WITH_SPECIFIED_SOURCE ( 'ANY', '', #46082, .NOT_KNOWN. ) ;
#17985=CIRCLE ( 'NONE', #40819, 3.982850737850967437 ) ;
#17987=DIRECTION ( 'NONE',  ( 1.224646799147353207E-16, 1.000000000000000000, -1.912410701131276611E-32 ) ) ;
#18033=APPLICATION_CONTEXT ( 'automotive_design' ) ;
#18044=DIRECTION ( 'NONE',  ( -1.000000000000000000, 1.224646799147353207E-16, -3.435970187611875923E-15 ) ) ;
#18056=AXIS2_PLACEMENT_3D ( 'NONE', #31670, #46691, #20096 ) ;
#18082=CONICAL_SURFACE ( 'NONE', #37742, 0.5560000000000009379, 0.06981317007976595157 ) ;
#18101=DIRECTION ( 'NONE',  ( -1.642720032068235908E-15, -0.8949343913984794119, 0.4461977533473619473 ) ) ;
#18170=ORIENTED_EDGE ( 'NONE', *, *, #19020, .F. ) ;
#18203=CIRCLE ( 'NONE', #14252, 1.250000000000001110 ) ;
#18333=CARTESIAN_POINT ( 'NONE',  ( -45.55409385541305767, -16.70920654474410938, 70.50000000000000000 ) ) ;
#18344=DIRECTION ( 'NONE',  ( 0.000000000000000000, -1.912410701131276611E-32, -1.000000000000000000 ) ) ;
#18365=DIRECTION ( 'NONE',  ( -0.4461977533475101065, -0.8949343913984055821, 2.835129006680928249E-16 ) ) ;
#18370=DIRECTION ( 'NONE',  ( -1.000000000000000000, 1.224646799147353207E-16, 5.551115123125782702E-17 ) ) ;
#18408=DIRECTION ( 'NONE',  ( 1.000000000000000000, -6.517531090241554163E-16, 3.534154189880001717E-15 ) ) ;
#18444=CARTESIAN_POINT ( 'NONE',  ( -45.92409385541306222, -14.90920654474410867, 70.50000000000000000 ) ) ;
#18476=CARTESIAN_POINT ( 'NONE',  ( -46.29409385541305255, -14.20920654474410760, 69.94787228701220272 ) ) ;
#18487=AXIS2_PLACEMENT_3D ( 'NONE', #33749, #41393, #37433 ) ;
#18565=LINE ( 'NONE', #19069, #15744 ) ;
#18619=CARTESIAN_POINT ( 'NONE',  ( -46.47622156840087371, -14.20920654474410760, 70.43449436244988249 ) ) ;
#18629=CARTESIAN_POINT ( 'NONE',  ( -45.37196614242555626, -14.20920654474410760, 70.87000000000000455 ) ) ;
#18676=DIRECTION ( 'NONE',  ( -1.423524324494147398E-15, 0.8949343913984055821, 0.4461977533475100510 ) ) ;
#18703=EDGE_CURVE ( 'NONE', #39770, #41197, #31470, .T. ) ;
#18734=DIRECTION ( 'NONE',  ( 0.4461977533473615032, -0.8949343913984796339, 0.000000000000000000 ) ) ;
#18773=AXIS2_PLACEMENT_3D ( 'NONE', #32318, #28615, #35740 ) ;
#18776=EDGE_CURVE ( 'NONE', #93, #18791, #29240, .T. ) ;
#18782=ORIENTED_EDGE ( 'NONE', *, *, #25344, .F. ) ;
#18791=VERTEX_POINT ( 'NONE', #40083 ) ;
#18820=EDGE_CURVE ( 'NONE', #12407, #34367, #32684, .T. ) ;
#18830=EDGE_LOOP ( 'NONE', ( #7809, #19861, #28938, #36874 ) ) ;
#18881=CARTESIAN_POINT ( 'NONE',  ( -45.92409385541306932, -16.70920654474410938, 70.13000000000000966 ) ) ;
#18882=CIRCLE ( 'NONE', #47212, 3.951441697420869481 ) ;
#18914=DIRECTION ( 'NONE',  ( 6.517531090241554163E-16, 1.000000000000000000, 1.799495156056576137E-30 ) ) ;
#18921=CARTESIAN_POINT ( 'NONE',  ( -45.55409385541306477, -14.20920654474410760, 71.05212771298751306 ) ) ;
#18932=EDGE_LOOP ( 'NONE', ( #31693, #43716 ) ) ;
#18945=DIRECTION ( 'NONE',  ( 2.342027643795563533E-48, 1.912410701131276611E-32, 1.000000000000000000 ) ) ;
#18954=VECTOR ( 'NONE', #12630, 1000.000000000000000 ) ;
#18960=CARTESIAN_POINT ( 'NONE',  ( -44.72480688026392670, -12.91120565595568692, 70.13000000000000966 ) ) ;
#19017=ORIENTED_EDGE ( 'NONE', *, *, #10152, .T. ) ;
#19020=EDGE_CURVE ( 'NONE', #12407, #31776, #45625, .T. ) ;
#19023=AXIS2_PLACEMENT_3D ( 'NONE', #39595, #46984, #9090 ) ;
#19069=CARTESIAN_POINT ( 'NONE',  ( -44.62409385541305795, -12.70920654474410760, 70.13000000000000966 ) ) ;
#19152=ORIENTED_EDGE ( 'NONE', *, *, #38199, .T. ) ;
#19173=ORIENTED_EDGE ( 'NONE', *, *, #2591, .T. ) ;
#19192=DIRECTION ( 'NONE',  ( 5.410999918679618404E-17, 0.000000000000000000, 1.000000000000000000 ) ) ;
#19289=DIRECTION ( 'NONE',  ( 0.000000000000000000, 0.000000000000000000, 1.000000000000000000 ) ) ;
#19297=VERTEX_POINT ( 'NONE', #37271 ) ;
#19320=DIRECTION ( 'NONE',  ( 0.000000000000000000, 0.000000000000000000, 1.000000000000000000 ) ) ;
#19419=CARTESIAN_POINT ( 'NONE',  ( -46.33910710821349710, -14.20920654474410760, 70.87000000000000455 ) ) ;
#19465=CARTESIAN_POINT ( 'NONE',  ( -46.29409385541305966, -16.70920654474410938, 70.50000000000000000 ) ) ;
#19484=AXIS2_PLACEMENT_3D ( 'NONE', #46947, #10261, #16891 ) ;
#19618=ORIENTED_EDGE ( 'NONE', *, *, #46783, .T. ) ;
#19652=CARTESIAN_POINT ( 'NONE',  ( -45.37196614242555626, -14.20920654474410760, 70.87000000000000455 ) ) ;
#19670=AXIS2_PLACEMENT_3D ( 'NONE', #24342, #46264, #39355 ) ;
#19764=CARTESIAN_POINT ( 'NONE',  ( -45.92409385541306222, -17.80920654474411435, 70.50000000000000000 ) ) ;
#19835=LINE ( 'NONE', #4095, #38758 ) ;
#19844=LINE ( 'NONE', #45942, #36413 ) ;
#19860=ORIENTED_EDGE ( 'NONE', *, *, #10359, .F. ) ;
#19861=ORIENTED_EDGE ( 'NONE', *, *, #10356, .F. ) ;
#19903=PRODUCT_DEFINITION_CONTEXT ( 'detailed design', #28121, 'design' ) ;
#20020=PLANE ( 'NONE',  #36022 ) ;
#20034=ORIENTED_EDGE ( 'NONE', *, *, #10152, .F. ) ;
#20096=DIRECTION ( 'NONE',  ( 0.000000000000000000, 0.000000000000000000, 1.000000000000000000 ) ) ;
#20129=DIRECTION ( 'NONE',  ( -1.000000000000000000, 1.224646799147353207E-16, -4.267285103686820140E-17 ) ) ;
#20178=EDGE_CURVE ( 'NONE', #17364, #39895, #23735, .T. ) ;
#20213=PLANE ( 'NONE',  #22584 ) ;
#20231=EDGE_CURVE ( 'NONE', #16774, #28537, #20515, .T. ) ;
#20246=CARTESIAN_POINT ( 'NONE',  ( -46.47622156840087371, -14.20920654474410760, 70.13000000000000966 ) ) ;
#20255=FACE_OUTER_BOUND ( 'NONE', #47838, .T. ) ;
#20286=CARTESIAN_POINT ( 'NONE',  ( -45.92409385541306222, -13.70421070448077039, 73.00000000000001421 ) ) ;
#20366=CIRCLE ( 'NONE', #4616, 1.250000000000001110 ) ;
#20371=CIRCLE ( 'NONE', #40026, 0.5560000000000009379 ) ;
#20422=DIRECTION ( 'NONE',  ( 3.484385612528001215E-15, 0.000000000000000000, -1.000000000000000000 ) ) ;
#20432=FACE_OUTER_BOUND ( 'NONE', #4481, .T. ) ;
#20452=CARTESIAN_POINT ( 'NONE',  ( -45.92409385541306222, -14.80920654474410902, 68.00000000000000000 ) ) ;
#20515=LINE ( 'NONE', #47096, #18954 ) ;
#20544=EDGE_LOOP ( 'NONE', ( #49, #24478, #48358, #6571 ) ) ;
#20581=AXIS2_PLACEMENT_3D ( 'NONE', #14113, #43479, #10224 ) ;
#20583=DIRECTION ( 'NONE',  ( 1.224646799147353207E-16, 1.000000000000000000, -1.912410701131276611E-32 ) ) ;
#20593=DIRECTION ( 'NONE',  ( 0.000000000000000000, 0.000000000000000000, 1.000000000000000000 ) ) ;
#20630=DIRECTION ( 'NONE',  ( 1.224646799147353207E-16, 1.000000000000000000, -1.912410701131276611E-32 ) ) ;
#20726=ADVANCED_FACE ( 'NONE', ( #41744 ), #14868, .T. ) ;
#20760=ORIENTED_EDGE ( 'NONE', *, *, #29449, .T. ) ;
#20772=EDGE_CURVE ( 'NONE', #37849, #1571, #17361, .T. ) ;
#20781=DIRECTION ( 'NONE',  ( 0.000000000000000000, -1.000000000000000000, 0.000000000000000000 ) ) ;
#20797=CIRCLE ( 'NONE', #4283, 3.982850737850970990 ) ;
#20832=TOROIDAL_SURFACE ( 'NONE', #48330, 1.350000000000000311, 0.1000000000000000056 ) ;
#20904=ORIENTED_EDGE ( 'NONE', *, *, #45803, .F. ) ;
#21031=AXIS2_PLACEMENT_3D ( 'NONE', #11374, #23436, #27364 ) ;
#21077=DIRECTION ( 'NONE',  ( -1.224646799147353207E-16, -1.000000000000000000, 1.912410701131276611E-32 ) ) ;
#21228=CARTESIAN_POINT ( 'NONE',  ( -45.55409385541306477, -12.76354662275040397, 71.04301729251712061 ) ) ;
#21234=DIRECTION ( 'NONE',  ( 5.551115123125782702E-17, 1.232595164407830946E-32, 1.000000000000000000 ) ) ;
#21238=ORIENTED_EDGE ( 'NONE', *, *, #44578, .T. ) ;
#21497=DIRECTION ( 'NONE',  ( -3.159776991290051445E-16, -1.000000000000000000, -6.457808579236824910E-31 ) ) ;
#21506=DIRECTION ( 'NONE',  ( 1.224646799147353207E-16, 1.000000000000000000, -1.912410701131276611E-32 ) ) ;
#21523=FACE_OUTER_BOUND ( 'NONE', #27089, .T. ) ;
#21564=ADVANCED_FACE ( 'NONE', ( #43750 ), #36334, .T. ) ;
#21572=CARTESIAN_POINT ( 'NONE',  ( -45.92409385541306932, -16.43194983366105077, 71.05609102496107710 ) ) ;
#21627=ORIENTED_EDGE ( 'NONE', *, *, #2315, .F. ) ;
#21646=ORIENTED_EDGE ( 'NONE', *, *, #9883, .T. ) ;
#21651=ORIENTED_EDGE ( 'NONE', *, *, #33744, .T. ) ;
#21714=CARTESIAN_POINT ( 'NONE',  ( -45.55409385541306477, -13.72754205882879042, 70.03986341317408915 ) ) ;
#21805=EDGE_CURVE ( 'NONE', #73, #19297, #2072, .T. ) ;
#21810=CARTESIAN_POINT ( 'NONE',  ( -45.92409385541306932, -16.70920654474410938, 70.50000000000000000 ) ) ;
#21839=EDGE_CURVE ( 'NONE', #11979, #16837, #38520, .T. ) ;
#21887=DIRECTION ( 'NONE',  ( 0.000000000000000000, 0.000000000000000000, 1.000000000000000000 ) ) ;
#21922=ADVANCED_FACE ( 'NONE', ( #28432 ), #18082, .F. ) ;
#21967=FACE_OUTER_BOUND ( 'NONE', #43637, .T. ) ;
#21996=CARTESIAN_POINT ( 'NONE',  ( -46.47622156840087371, -14.20920654474410760, 70.13000000000000966 ) ) ;
#22084=PLANE ( 'NONE',  #5466 ) ;
#22110=CARTESIAN_POINT ( 'NONE',  ( -46.47622156840087371, -14.20920654474410760, 70.13000000000000966 ) ) ;
#22122=VERTEX_POINT ( 'NONE', #12850 ) ;
#22127=ADVANCED_FACE ( 'NONE', ( #38956 ), #5231, .F. ) ;
#22206=CARTESIAN_POINT ( 'NONE',  ( -45.55409385541305767, -13.24559821555319061, 69.99777223794900749 ) ) ;
#22242=LINE ( 'NONE', #3514, #39873 ) ;
#22276=CARTESIAN_POINT ( 'NONE',  ( -46.29409385541305255, -14.20920654474410760, 70.08498674719956512 ) ) ;
#22278=CARTESIAN_POINT ( 'NONE',  ( -45.92409385541306222, -14.20920654474410760, 70.50000000000000000 ) ) ;
#22290=DIRECTION ( 'NONE',  ( 6.517531090241554163E-16, 1.000000000000000000, 1.799495156056576137E-30 ) ) ;
#22309=DIRECTION ( 'NONE',  ( 0.4461977533475104396, 0.8949343913984053600, 0.000000000000000000 ) ) ;
#22325=ORIENTED_EDGE ( 'NONE', *, *, #28446, .T. ) ;
#22386=DIRECTION ( 'NONE',  ( -2.867370864192053523E-15, -0.4461977533475100510, 0.8949343913984055821 ) ) ;
#22442=FACE_OUTER_BOUND ( 'NONE', #10038, .T. ) ;
#22491=EDGE_CURVE ( 'NONE', #38900, #9803, #29612, .T. ) ;
#22517=ORIENTED_EDGE ( 'NONE', *, *, #18776, .T. ) ;
#22561=EDGE_CURVE ( 'NONE', #45017, #24736, #36640, .T. ) ;
#22569=VERTEX_POINT ( 'NONE', #32483 ) ;
#22584=AXIS2_PLACEMENT_3D ( 'NONE', #13290, #35226, #28084 ) ;
#22608=FACE_OUTER_BOUND ( 'NONE', #16681, .T. ) ;
#22631=ADVANCED_FACE ( 'NONE', ( #29510 ), #40834, .T. ) ;
#22660=CIRCLE ( 'NONE', #1417, 3.999999999999996447 ) ;
#22667=CARTESIAN_POINT ( 'NONE',  ( -46.47622156840087371, -14.20920654474410760, 70.13000000000000966 ) ) ;
#22679=CIRCLE ( 'NONE', #32104, 3.951441697420869481 ) ;
#22727=ADVANCED_FACE ( 'NONE', ( #12498 ), #38841, .F. ) ;
#22797=DIRECTION ( 'NONE',  ( -1.000000000000000000, 3.159776991290051445E-16, -3.534154189880001717E-15 ) ) ;
#22806=DIRECTION ( 'NONE',  ( 5.551115123125782702E-17, 1.232595164407830946E-32, 1.000000000000000000 ) ) ;
#22837=VECTOR ( 'NONE', #3401, 1000.000000000000000 ) ;
#22844=CARTESIAN_POINT ( 'NONE',  ( -45.92409385541306222, -14.90920654474410867, 71.75000000000001421 ) ) ;
#22882=CARTESIAN_POINT ( 'NONE',  ( -45.94606420501752098, -14.19714313411900264, 69.94185769334995939 ) ) ;
#23077=ORIENTED_EDGE ( 'NONE', *, *, #24775, .T. ) ;
#23146=CARTESIAN_POINT ( 'NONE',  ( -45.92409385541293432, 985.6101381041504510, 70.50000000000000000 ) ) ;
#23162=EDGE_CURVE ( 'NONE', #28374, #46725, #28797, .T. ) ;
#23311=DIRECTION ( 'NONE',  ( 0.000000000000000000, 0.000000000000000000, 1.000000000000000000 ) ) ;
#23346=DIRECTION ( 'NONE',  ( -5.551115123125782702E-17, -1.232595164407830946E-32, -1.000000000000000000 ) ) ;
#23403=CARTESIAN_POINT ( 'NONE',  ( -45.92409385541306932, -16.43194983366065287, 69.94390897503836868 ) ) ;
#23436=DIRECTION ( 'NONE',  ( 1.224646799147353207E-16, 1.000000000000000000, -1.912410701131276611E-32 ) ) ;
#23492=CARTESIAN_POINT ( 'NONE',  ( -45.38107656289594871, -12.76354662275040219, 70.87000000000000455 ) ) ;
#23534=( GEOMETRIC_REPRESENTATION_CONTEXT ( 3 ) GLOBAL_UNCERTAINTY_ASSIGNED_CONTEXT ( ( #42069 ) ) GLOBAL_UNIT_ASSIGNED_CONTEXT ( ( #14481, #40608, #3683 ) ) REPRESENTATION_CONTEXT ( 'NONE', 'WORKASPACE' ) );
#23620=EDGE_LOOP ( 'NONE', ( #5901, #1551, #3891, #16980 ) ) ;
#23657=DIRECTION ( 'NONE',  ( -0.8949343913984795229, -0.4461977533473618918, 4.967883834297468681E-17 ) ) ;
#23678=VECTOR ( 'NONE', #18365, 1000.000000000000114 ) ;
#23734=DIRECTION ( 'NONE',  ( 1.224646799147353207E-16, 1.000000000000000000, -1.912410701131276611E-32 ) ) ;
#23735=LINE ( 'NONE', #38729, #47983 ) ;
#23752=AXIS2_PLACEMENT_3D ( 'NONE', #21572, #36795, #36551 ) ;
#23757=VECTOR ( 'NONE', #29168, 1000.000000000000000 ) ;
#23765=AXIS2_PLACEMENT_3D ( 'NONE', #43689, #12660, #39005 ) ;
#23783=DIRECTION ( 'NONE',  ( 0.000000000000000000, -1.000000000000000000, 0.000000000000000000 ) ) ;
#23792=LINE ( 'NONE', #11980, #6401 ) ;
#23963=ORIENTED_EDGE ( 'NONE', *, *, #23162, .F. ) ;
#23967=AXIS2_PLACEMENT_3D ( 'NONE', #39043, #31421, #46454 ) ;
#23984=DIRECTION ( 'NONE',  ( 1.000000000000000000, -6.517531090241554163E-16, 3.534154189880001717E-15 ) ) ;
#23994=ORIENTED_EDGE ( 'NONE', *, *, #17378, .F. ) ;
#24040=AXIS2_PLACEMENT_3D ( 'NONE', #41176, #40679, #3748 ) ;
#24109=DIRECTION ( 'NONE',  ( -1.000000000000000000, 3.159776991290051445E-16, -3.534154189880001717E-15 ) ) ;
#24149=ORIENTED_EDGE ( 'NONE', *, *, #10356, .T. ) ;
#24190=DIRECTION ( 'NONE',  ( -1.224646799147353207E-16, -1.000000000000000000, 1.912410701131276611E-32 ) ) ;
#24243=VECTOR ( 'NONE', #11369, 1000.000000000000114 ) ;
#24342=CARTESIAN_POINT ( 'NONE',  ( -45.92409385541306222, -14.20920654474410760, 70.50000000000000000 ) ) ;
#24478=ORIENTED_EDGE ( 'NONE', *, *, #25344, .T. ) ;
#24496=DIRECTION ( 'NONE',  ( -1.000000000000000000, 1.224646799147353207E-16, 5.551115123125782702E-17 ) ) ;
#24503=ADVANCED_FACE ( 'NONE', ( #28055 ), #43080, .T. ) ;
#24522=MECHANICAL_DESIGN_GEOMETRIC_PRESENTATION_REPRESENTATION('',(#45756),#27628);
#24539=CARTESIAN_POINT ( 'NONE',  ( -45.92409385541306222, -14.20920654474410760, 70.50000000000000000 ) ) ;
#24544=EDGE_LOOP ( 'NONE', ( #957, #34223, #24676 ) ) ;
#24624=EDGE_CURVE ( 'NONE', #11860, #22569, #22679, .T. ) ;
#24663=FILL_AREA_STYLE ('',( #13298 ) ) ;
#24676=ORIENTED_EDGE ( 'NONE', *, *, #21805, .T. ) ;
#24725=ORIENTED_EDGE ( 'NONE', *, *, #24624, .T. ) ;
#24736=VERTEX_POINT ( 'NONE', #35329 ) ;
#24767=ORIENTED_EDGE ( 'NONE', *, *, #35850, .T. ) ;
#24775=EDGE_CURVE ( 'NONE', #40286, #32734, #46273, .T. ) ;
#24811=DIRECTION ( 'NONE',  ( -4.267285103686820140E-17, 1.935130192142698731E-16, 1.000000000000000000 ) ) ;
#24960=FACE_OUTER_BOUND ( 'NONE', #11340, .T. ) ;
#24971=AXIS2_PLACEMENT_3D ( 'NONE', #22667, #37665, #3960 ) ;
#24973=DIRECTION ( 'NONE',  ( 0.000000000000000000, 0.000000000000000000, -1.000000000000000000 ) ) ;
#24996=ORIENTED_EDGE ( 'NONE', *, *, #11533, .T. ) ;
#25076=( BOUNDED_CURVE ( )  B_SPLINE_CURVE ( 3, ( #11296, #44796, #22882, #45050 ),
 .UNSPECIFIED., .F., .F. ) 
 B_SPLINE_CURVE_WITH_KNOTS ( ( 4, 4 ),
 ( 6.147240100468662760, 6.419130513890517697 ),
 .UNSPECIFIED. ) 
 CURVE ( )  GEOMETRIC_REPRESENTATION_ITEM ( )  RATIONAL_B_SPLINE_CURVE ( ( 1.000000000000000000, 0.9938491152766115722, 0.9938491152766115722, 1.000000000000000000 ) ) 
 REPRESENTATION_ITEM ( '' )  );
#25098=DIRECTION ( 'NONE',  ( 0.000000000000000000, 0.000000000000000000, 1.000000000000000000 ) ) ;
#25108=CARTESIAN_POINT ( 'NONE',  ( -45.92409385541306222, 12.69079345525585545, 70.50000000000000000 ) ) ;
#25138=( NAMED_UNIT ( * ) SI_UNIT ( $, .STERADIAN. ) SOLID_ANGLE_UNIT ( ) );
#25171=CARTESIAN_POINT ( 'NONE',  ( -45.92409385541306932, -16.70920654474410938, 70.50000000000000000 ) ) ;
#25187=DIRECTION ( 'NONE',  ( 1.000000000000000000, -1.224646799147353207E-16, 4.267285103686821372E-17 ) ) ;
#25196=VECTOR ( 'NONE', #8301, 1000.000000000000000 ) ;
#25267=ADVANCED_FACE ( 'NONE', ( #20255 ), #43408, .T. ) ;
#25319=LINE ( 'NONE', #18629, #13426 ) ;
#25334=ORIENTED_EDGE ( 'NONE', *, *, #25987, .F. ) ;
#25344=EDGE_CURVE ( 'NONE', #46725, #32734, #2023, .T. ) ;
#25380=CARTESIAN_POINT ( 'NONE',  ( -45.92409385541306222, -13.51240245935757578, 70.50000000000000000 ) ) ;
#25382=VERTEX_POINT ( 'NONE', #3230 ) ;
#25385=ORIENTED_EDGE ( 'NONE', *, *, #48261, .F. ) ;
#25461=DIRECTION ( 'NONE',  ( 0.8949343913984054710, -0.4461977533475101065, -3.119193279067933041E-16 ) ) ;
#25506=EDGE_CURVE ( 'NONE', #46725, #28374, #39236, .T. ) ;
#25525=DIRECTION ( 'NONE',  ( -1.224646799147353207E-16, -1.000000000000000000, 1.935130192142698731E-16 ) ) ;
#25600=FACE_OUTER_BOUND ( 'NONE', #35379, .T. ) ;
#25621=AXIS2_PLACEMENT_3D ( 'NONE', #23146, #34697, #19192 ) ;
#25658=DIRECTION ( 'NONE',  ( 0.000000000000000000, 0.000000000000000000, 1.000000000000000000 ) ) ;
#25700=AXIS2_PLACEMENT_3D ( 'NONE', #21996, #36991, #2786 ) ;
#25706=ORIENTED_EDGE ( 'NONE', *, *, #33310, .F. ) ;
#25789=ORIENTED_EDGE ( 'NONE', *, *, #37540, .T. ) ;
#25845=CIRCLE ( 'NONE', #1480, 2.404255319148937531 ) ;
#25886=CARTESIAN_POINT ( 'NONE',  ( -46.42632161746406894, -13.24559821555319239, 70.13000000000000966 ) ) ;
#25905=PLANE ( 'NONE',  #1138 ) ;
#25987=EDGE_CURVE ( 'NONE', #40177, #3121, #14613, .T. ) ;
#26023=DIRECTION ( 'NONE',  ( 5.551115123125782702E-17, 1.232595164407830946E-32, 1.000000000000000000 ) ) ;
#26026=CARTESIAN_POINT ( 'NONE',  ( -45.92409385541306222, -14.90920654474410867, 71.85000000000000853 ) ) ;
#26039=CARTESIAN_POINT ( 'NONE',  ( -47.12338083056222615, -12.91120565595569580, 70.13000000000000966 ) ) ;
#26040=ORIENTED_EDGE ( 'NONE', *, *, #31234, .T. ) ;
#26049=ADVANCED_FACE ( 'NONE', ( #17873 ), #22084, .T. ) ;
#26059=CARTESIAN_POINT ( 'NONE',  ( -45.92409385541306222, -14.20920654474410760, 70.50000000000000000 ) ) ;
#26110=ORIENTED_EDGE ( 'NONE', *, *, #42657, .F. ) ;
#26204=CARTESIAN_POINT ( 'NONE',  ( -45.36595154876284397, -14.19714313411803985, 70.47802965039466017 ) ) ;
#26371=DIRECTION ( 'NONE',  ( 1.000000000000000000, -6.517531090241554163E-16, 3.534154189880001717E-15 ) ) ;
#26411=LINE ( 'NONE', #41422, #8789 ) ;
#26413=AXIS2_PLACEMENT_3D ( 'NONE', #6483, #21506, #45622 ) ;
#26416=ORIENTED_EDGE ( 'NONE', *, *, #2591, .F. ) ;
#26513=DIRECTION ( 'NONE',  ( 0.000000000000000000, -1.000000000000000000, 0.000000000000000000 ) ) ;
#26549=AXIS2_PLACEMENT_3D ( 'NONE', #2527, #3483, #36957 ) ;
#26570=ORIENTED_EDGE ( 'NONE', *, *, #17243, .T. ) ;
#26591=CIRCLE ( 'NONE', #48582, 3.999999999999996447 ) ;
#26743=ORIENTED_EDGE ( 'NONE', *, *, #6033, .F. ) ;
#26745=DIRECTION ( 'NONE',  ( 0.000000000000000000, 0.000000000000000000, 1.000000000000000000 ) ) ;
#26795=AXIS2_PLACEMENT_3D ( 'NONE', #15883, #30928, #23783 ) ;
#26847=CIRCLE ( 'NONE', #40232, 2.404255319148937531 ) ;
#26871=CONICAL_SURFACE ( 'NONE', #20581, 0.5560000000000009379, 0.06981317007976595157 ) ;
#26986=LINE ( 'NONE', #35086, #9381 ) ;
#27032=VERTEX_POINT ( 'NONE', #16597 ) ;
#27054=ORIENTED_EDGE ( 'NONE', *, *, #35171, .T. ) ;
#27089=EDGE_LOOP ( 'NONE', ( #29384, #7733, #33639 ) ) ;
#27191=TOROIDAL_SURFACE ( 'NONE', #47614, 1.350000000000000311, 0.1000000000000000056 ) ;
#27229=ORIENTED_EDGE ( 'NONE', *, *, #18820, .F. ) ;
#27279=CARTESIAN_POINT ( 'NONE',  ( -46.47622156840087371, -14.20920654474410760, 70.13000000000000966 ) ) ;
#27364=DIRECTION ( 'NONE',  ( 2.342027643795563533E-48, 1.912410701131276611E-32, 1.000000000000000000 ) ) ;
#27548=CARTESIAN_POINT ( 'NONE',  ( -45.92409385541306222, -13.70421070448076861, 70.50000000000000000 ) ) ;
#27624=ADVANCED_FACE ( 'NONE', ( #15495 ), #10243, .F. ) ;
#27628=( GEOMETRIC_REPRESENTATION_CONTEXT ( 3 ) GLOBAL_UNCERTAINTY_ASSIGNED_CONTEXT ( ( #1671 ) ) GLOBAL_UNIT_ASSIGNED_CONTEXT ( ( #47548, #5937, #25138 ) ) REPRESENTATION_CONTEXT ( 'NONE', 'WORKASPACE' ) );
#27684=EDGE_CURVE ( 'NONE', #37849, #45322, #18882, .T. ) ;
#27711=EDGE_LOOP ( 'NONE', ( #20034, #26570, #6287 ) ) ;
#27731=ORIENTED_EDGE ( 'NONE', *, *, #6339, .T. ) ;
#27745=B_SPLINE_CURVE_WITH_KNOTS ( 'NONE', 3,
 ( #29578, #44608, #25886, #40901 ),
 .UNSPECIFIED., .F., .F.,
 ( 4, 4 ),
 ( 0.001310108020966226300, 0.002761379516309090103 ),
 .UNSPECIFIED. ) ;
#27935=EDGE_CURVE ( 'NONE', #16774, #8094, #11042, .T. ) ;
#27975=ORIENTED_EDGE ( 'NONE', *, *, #40438, .F. ) ;
#28012=EDGE_CURVE ( 'NONE', #3121, #14597, #35618, .T. ) ;
#28052=CIRCLE ( 'NONE', #35152, 2.404255319148937531 ) ;
#28055=FACE_OUTER_BOUND ( 'NONE', #23620, .T. ) ;
#28084=DIRECTION ( 'NONE',  ( 0.4461977533475101065, 0.8949343913984054710, -2.476895096512112418E-17 ) ) ;
#28121=APPLICATION_CONTEXT ( 'automotive_design' ) ;
#28184=DIRECTION ( 'NONE',  ( 1.224646799147353207E-16, 1.000000000000000000, -1.912410701131276611E-32 ) ) ;
#28207=CIRCLE ( 'NONE', #13238, 3.951441697420975618 ) ;
#28293=DIRECTION ( 'NONE',  ( 1.224646799147352961E-16, 1.000000000000000000, -5.292884291094200710E-16 ) ) ;
#28317=DIRECTION ( 'NONE',  ( 0.000000000000000000, 0.000000000000000000, 1.000000000000000000 ) ) ;
#28341=DIRECTION ( 'NONE',  ( 0.000000000000000000, 0.000000000000000000, 1.000000000000000000 ) ) ;
#28345=AXIS2_PLACEMENT_3D ( 'NONE', #20246, #24190, #16049 ) ;
#28350=VERTEX_POINT ( 'NONE', #10734 ) ;
#28354=SURFACE_STYLE_USAGE ( .BOTH. , #28822 ) ;
#28374=VERTEX_POINT ( 'NONE', #42001 ) ;
#28412=CARTESIAN_POINT ( 'NONE',  ( -46.29409385541305255, -13.24559821555319239, 69.99777223794899328 ) ) ;
#28432=FACE_OUTER_BOUND ( 'NONE', #43146, .T. ) ;
#28446=EDGE_CURVE ( 'NONE', #11860, #11979, #856, .T. ) ;
#28503=LINE ( 'NONE', #40307, #7811 ) ;
#28537=VERTEX_POINT ( 'NONE', #44855 ) ;
#28539=FACE_OUTER_BOUND ( 'NONE', #13256, .T. ) ;
#28551=ORIENTED_EDGE ( 'NONE', *, *, #2640, .F. ) ;
#28565=DIRECTION ( 'NONE',  ( 0.4461977533473618363, -0.8949343913984794119, 4.927189484408733560E-16 ) ) ;
#28581=DIRECTION ( 'NONE',  ( 1.224646799147353207E-16, 1.000000000000000000, -1.912410701131276611E-32 ) ) ;
#28615=DIRECTION ( 'NONE',  ( -4.267285103686820140E-17, 1.935130192142698731E-16, 1.000000000000000000 ) ) ;
#28739=DIRECTION ( 'NONE',  ( 0.000000000000000000, 0.000000000000000000, 1.000000000000000000 ) ) ;
#28797=CIRCLE ( 'NONE', #41371, 2.500000000000002220 ) ;
#28822=SURFACE_SIDE_STYLE ('',( #35714 ) ) ;
#28823=DIRECTION ( 'NONE',  ( 0.000000000000000000, 0.000000000000000000, 1.000000000000000000 ) ) ;
#28831=AXIS2_PLACEMENT_3D ( 'NONE', #18881, #8069, #26513 ) ;
#28869=DIRECTION ( 'NONE',  ( -1.224646799147353207E-16, -1.000000000000000000, 1.912410701131276611E-32 ) ) ;
#28938=ORIENTED_EDGE ( 'NONE', *, *, #4246, .T. ) ;
#28976=AXIS2_PLACEMENT_3D ( 'NONE', #14823, #25461, #34047 ) ;
#29031=AXIS2_PLACEMENT_3D ( 'NONE', #29301, #44568, #33698 ) ;
#29060=ORIENTED_EDGE ( 'NONE', *, *, #7011, .T. ) ;
#29102=DIRECTION ( 'NONE',  ( 0.000000000000000000, 1.000000000000000000, 0.000000000000000000 ) ) ;
#29168=DIRECTION ( 'NONE',  ( -3.485387654165294196E-16, 2.355958133329952458E-32, -1.000000000000000000 ) ) ;
#29178=AXIS2_PLACEMENT_3D ( 'NONE', #9251, #20583, #12445 ) ;
#29233=ORIENTED_EDGE ( 'NONE', *, *, #44320, .F. ) ;
#29240=LINE ( 'NONE', #40549, #39307 ) ;
#29301=CARTESIAN_POINT ( 'NONE',  ( 0.000000000000000000, 0.000000000000000000, 0.000000000000000000 ) ) ;
#29304=ORIENTED_EDGE ( 'NONE', *, *, #37540, .F. ) ;
#29317=EDGE_CURVE ( 'NONE', #35836, #93, #41519, .T. ) ;
#29384=ORIENTED_EDGE ( 'NONE', *, *, #40346, .F. ) ;
#29414=LINE ( 'NONE', #47414, #42802 ) ;
#29432=CARTESIAN_POINT ( 'NONE',  ( -45.92409385541306222, -14.20920654474410760, 69.94400000000000261 ) ) ;
#29433=CIRCLE ( 'NONE', #7457, 0.09999999999999939493 ) ;
#29440=EDGE_CURVE ( 'NONE', #41576, #10249, #37818, .T. ) ;
#29449=EDGE_CURVE ( 'NONE', #41197, #14597, #23792, .T. ) ;
#29487=CARTESIAN_POINT ( 'NONE',  ( -46.47622156840087371, -14.20920654474410760, 70.56550563755013172 ) ) ;
#29510=FACE_OUTER_BOUND ( 'NONE', #35131, .T. ) ;
#29564=ADVANCED_FACE ( 'NONE', ( #43229 ), #26871, .F. ) ;
#29578=CARTESIAN_POINT ( 'NONE',  ( -46.33910710821349710, -14.20920654474410760, 70.13000000000000966 ) ) ;
#29594=EDGE_CURVE ( 'NONE', #93, #7630, #47410, .T. ) ;
#29612=CIRCLE ( 'NONE', #9936, 3.951441697420975618 ) ;
#29651=AXIS2_PLACEMENT_3D ( 'NONE', #30863, #12365, #12845 ) ;
#29756=CONICAL_SURFACE ( 'NONE', #3783, 0.5560000000000009379, 0.06981317007976595157 ) ;
#29777=DIRECTION ( 'NONE',  ( -5.551115123125782702E-17, -1.232595164407830946E-32, -1.000000000000000000 ) ) ;
#29801=ORIENTED_EDGE ( 'NONE', *, *, #37779, .F. ) ;
#29807=EDGE_LOOP ( 'NONE', ( #10920, #16282, #15985, #7678 ) ) ;
#29924=DIRECTION ( 'NONE',  ( 0.000000000000000000, 0.000000000000000000, 1.000000000000000000 ) ) ;
#29963=CARTESIAN_POINT ( 'NONE',  ( -47.22409385541305937, -12.70920654474410760, 70.87000000000000455 ) ) ;
#30123=ADVANCED_FACE ( 'NONE', ( #12523 ), #13485, .T. ) ;
#30131=FACE_OUTER_BOUND ( 'NONE', #32251, .T. ) ;
#30173=DIRECTION ( 'NONE',  ( 0.000000000000000000, 0.000000000000000000, 1.000000000000000000 ) ) ;
#30185=DIRECTION ( 'NONE',  ( 3.484385612528001215E-15, 0.000000000000000000, -1.000000000000000000 ) ) ;
#30211=DIRECTION ( 'NONE',  ( 1.224646799147353207E-16, 1.000000000000000000, -1.912410701131276611E-32 ) ) ;
#30221=DIRECTION ( 'NONE',  ( 0.000000000000000000, 0.000000000000000000, 1.000000000000000000 ) ) ;
#30229=ADVANCED_FACE ( 'NONE', ( #42815 ), #35166, .T. ) ;
#30247=LINE ( 'NONE', #44293, #11151 ) ;
#30254=EDGE_LOOP ( 'NONE', ( #3417, #31417 ) ) ;
#30330=CARTESIAN_POINT ( 'NONE',  ( -45.92409385541306222, -14.80920654474410902, 70.50000000000000000 ) ) ;
#30368=CONICAL_SURFACE ( 'NONE', #25621, 3077.683537175336824, 1.256637061435925240 ) ;
#30449=VERTEX_POINT ( 'NONE', #22276 ) ;
#30522=DIRECTION ( 'NONE',  ( 1.224646799147353207E-16, 1.000000000000000000, -1.912410701131276611E-32 ) ) ;
#30557=CARTESIAN_POINT ( 'NONE',  ( -45.92409385541306222, -14.20920654474410760, 70.50000000000000000 ) ) ;
#30605=CARTESIAN_POINT ( 'NONE',  ( -46.29409385541305966, -12.76354662275040219, 71.04301729251712061 ) ) ;
#30647=DIRECTION ( 'NONE',  ( -5.551115123125782702E-17, -1.232595164407830946E-32, -1.000000000000000000 ) ) ;
#30822=ORIENTED_EDGE ( 'NONE', *, *, #16669, .T. ) ;
#30829=CIRCLE ( 'NONE', #23765, 0.6570903894995150374 ) ;
#30838=VECTOR ( 'NONE', #11177, 1000.000000000000114 ) ;
#30863=CARTESIAN_POINT ( 'NONE',  ( -45.92409385541306932, -12.76354662275040042, 70.50000000000000000 ) ) ;
#30875=CARTESIAN_POINT ( 'NONE',  ( -46.47622156840087371, -14.20920654474410760, 70.13000000000000966 ) ) ;
#30886=PLANE ( 'NONE',  #10908 ) ;
#30897=DIRECTION ( 'NONE',  ( 1.224646799147353207E-16, 1.000000000000000000, -1.912410701131276611E-32 ) ) ;
#30928=DIRECTION ( 'NONE',  ( -4.267285103686820140E-17, 1.935130192142698484E-16, 1.000000000000000000 ) ) ;
#30980=ORIENTED_EDGE ( 'NONE', *, *, #44320, .T. ) ;
#31073=EDGE_LOOP ( 'NONE', ( #9214, #38659, #29801, #25334 ) ) ;
#31132=DIRECTION ( 'NONE',  ( 1.224646799147353207E-16, 1.000000000000000000, -1.912410701131276611E-32 ) ) ;
#31165=DIRECTION ( 'NONE',  ( 5.551115123125782702E-17, 1.232595164407830946E-32, 1.000000000000000000 ) ) ;
#31197=LINE ( 'NONE', #34878, #13068 ) ;
#31225=CARTESIAN_POINT ( 'NONE',  ( -46.33910710821349710, -14.20920654474410760, 70.87000000000000455 ) ) ;
#31234=EDGE_CURVE ( 'NONE', #16837, #16407, #11076, .T. ) ;
#31250=ORIENTED_EDGE ( 'NONE', *, *, #36176, .T. ) ;
#31317=DIRECTION ( 'NONE',  ( 0.000000000000000000, 0.000000000000000000, 1.000000000000000000 ) ) ;
#31367=CARTESIAN_POINT ( 'NONE',  ( -45.90217435822630421, -14.20017296387473138, 71.05663168951063824 ) ) ;
#31417=ORIENTED_EDGE ( 'NONE', *, *, #47060, .F. ) ;
#31421=DIRECTION ( 'NONE',  ( 1.224646799147353207E-16, 1.000000000000000000, -1.912410701131276611E-32 ) ) ;
#31470=CIRCLE ( 'NONE', #19670, 0.5560000000000009379 ) ;
#31670=CARTESIAN_POINT ( 'NONE',  ( -45.92409385541306222, -14.20920654474410760, 70.50000000000000000 ) ) ;
#31693=ORIENTED_EDGE ( 'NONE', *, *, #8954, .T. ) ;
#31713=ORIENTED_EDGE ( 'NONE', *, *, #12149, .F. ) ;
#31776=VERTEX_POINT ( 'NONE', #35481 ) ;
#31829=CIRCLE ( 'NONE', #23967, 0.6570903894995150374 ) ;
#31912=EDGE_LOOP ( 'NONE', ( #18170, #40032, #31936 ) ) ;
#31936=ORIENTED_EDGE ( 'NONE', *, *, #10359, .T. ) ;
#31949=CARTESIAN_POINT ( 'NONE',  ( -46.46711114793018282, -12.76354662275040042, 70.87000000000000455 ) ) ;
#31956=CARTESIAN_POINT ( 'NONE',  ( -46.48223616206310993, -14.19714313411900619, 70.47802965039554124 ) ) ;
#31971=MANIFOLD_SOLID_BREP ( 'Stock-MAS-175-1', #36174 ) ;
#31998=CIRCLE ( 'NONE', #32798, 3.982850737850970990 ) ;
#32056=ORIENTED_EDGE ( 'NONE', *, *, #43115, .T. ) ;
#32062=CARTESIAN_POINT ( 'NONE',  ( -45.92409385541306932, -16.70920654474410938, 70.50000000000000000 ) ) ;
#32104=AXIS2_PLACEMENT_3D ( 'NONE', #11467, #33359, #22309 ) ;
#32184=ADVANCED_FACE ( 'NONE', ( #28539 ), #5885, .T. ) ;
#32251=EDGE_LOOP ( 'NONE', ( #12291, #39086, #44390, #16065, #17491, #2826 ) ) ;
#32287=EDGE_CURVE ( 'NONE', #73, #7134, #30247, .T. ) ;
#32318=CARTESIAN_POINT ( 'NONE',  ( -45.37196614242555626, -14.20920654474410760, 70.13000000000000966 ) ) ;
#32339=FACE_OUTER_BOUND ( 'NONE', #27711, .T. ) ;
#32474=EDGE_LOOP ( 'NONE', ( #31713, #20904 ) ) ;
#32483=CARTESIAN_POINT ( 'NONE',  ( -44.71706047250183502, -12.89566876303302756, 70.50000000000000000 ) ) ;
#32500=ORIENTED_EDGE ( 'NONE', *, *, #6339, .F. ) ;
#32528=ORIENTED_EDGE ( 'NONE', *, *, #11093, .T. ) ;
#32560=CARTESIAN_POINT ( 'NONE',  ( -46.29409385541305966, -14.20920654474410760, 71.05212771298751306 ) ) ;
#32624=ORIENTED_EDGE ( 'NONE', *, *, #38199, .F. ) ;
#32640=ORIENTED_EDGE ( 'NONE', *, *, #32287, .T. ) ;
#32650=EDGE_CURVE ( 'NONE', #43290, #16407, #17427, .T. ) ;
#32652=ORIENTED_EDGE ( 'NONE', *, *, #16669, .F. ) ;
#32667=DIRECTION ( 'NONE',  ( 1.224646799147353207E-16, 1.000000000000000000, -1.912410701131276611E-32 ) ) ;
#32684=LINE ( 'NONE', #36598, #791 ) ;
#32734=VERTEX_POINT ( 'NONE', #11218 ) ;
#32762=VERTEX_POINT ( 'NONE', #29432 ) ;
#32787=CARTESIAN_POINT ( 'NONE',  ( -45.55409385541305767, -14.20920654474410760, 70.08498674719956512 ) ) ;
#32798=AXIS2_PLACEMENT_3D ( 'NONE', #9695, #23984, #36007 ) ;
#32877=EDGE_LOOP ( 'NONE', ( #37604, #32056, #29304 ) ) ;
#32947=DIRECTION ( 'NONE',  ( 1.224646799147353207E-16, 1.000000000000000000, -1.912410701131276611E-32 ) ) ;
#32968=EDGE_CURVE ( 'NONE', #40286, #2125, #7353, .T. ) ;
#33016=CARTESIAN_POINT ( 'NONE',  ( -45.55409385541305767, -12.76354662275040219, 69.95698270748289360 ) ) ;
#33055=AXIS2_PLACEMENT_3D ( 'NONE', #18333, #22797, #30185 ) ;
#33109=COLOUR_RGB ( '', 0.72549020, 0.75294118, 0.79215686) ;
#33120=B_SPLINE_CURVE_WITH_KNOTS ( 'NONE', 3,
 ( #15584, #1555, #42199, #23492 ),
 .UNSPECIFIED., .F., .F.,
 ( 4, 4 ),
 ( 0.001310108020964424790, 0.002761379516307284256 ),
 .UNSPECIFIED. ) ;
#33197=CARTESIAN_POINT ( 'NONE',  ( -45.38107656289594871, -12.76354662275040219, 70.87000000000000455 ) ) ;
#33249=DIRECTION ( 'NONE',  ( 1.000000000000000000, 0.000000000000000000, 0.000000000000000000 ) ) ;
#33288=CARTESIAN_POINT ( 'NONE',  ( -45.55409385541305767, -14.20920654474410760, 69.94787228701220272 ) ) ;
#33310=EDGE_CURVE ( 'NONE', #22122, #39770, #19835, .T. ) ;
#33354=CARTESIAN_POINT ( 'NONE',  ( -45.55409385541305767, -12.70920654474410760, 69.20000000000001705 ) ) ;
#33359=DIRECTION ( 'NONE',  ( 0.8949343913984054710, -0.4461977533475101065, -3.119193279067933041E-16 ) ) ;
#33429=EDGE_LOOP ( 'NONE', ( #8325, #42609, #43238, #21651, #5803, #36119, #12594, #37161, #32528, #2550, #30980 ) ) ;
#33486=CARTESIAN_POINT ( 'NONE',  ( -45.36800283045199933, -16.43194983366105077, 70.50000000000000000 ) ) ;
#33639=ORIENTED_EDGE ( 'NONE', *, *, #4121, .F. ) ;
#33698=DIRECTION ( 'NONE',  ( 1.000000000000000000, 0.000000000000000000, 0.000000000000000000 ) ) ;
#33744=EDGE_CURVE ( 'NONE', #31776, #25382, #34073, .T. ) ;
#33749=CARTESIAN_POINT ( 'NONE',  ( -46.47622156840087371, -14.20920654474410760, 70.87000000000000455 ) ) ;
#33980=ORIENTED_EDGE ( 'NONE', *, *, #43115, .F. ) ;
#34015=DIRECTION ( 'NONE',  ( -1.000000000000000000, 1.224646799147353207E-16, -3.435970187611875923E-15 ) ) ;
#34047=DIRECTION ( 'NONE',  ( 0.4461977533475104396, 0.8949343913984053600, 0.000000000000000000 ) ) ;
#34073=CIRCLE ( 'NONE', #15995, 0.5560000000000009379 ) ;
#34223=ORIENTED_EDGE ( 'NONE', *, *, #32287, .F. ) ;
#34235=CARTESIAN_POINT ( 'NONE',  ( -45.92409385541306222, -14.80920654474410725, 70.50000000000000000 ) ) ;
#34306=AXIS2_PLACEMENT_3D ( 'NONE', #18921, #48712, #7120 ) ;
#34307=CARTESIAN_POINT ( 'NONE',  ( -46.47622156840087371, -14.20920654474410760, 70.13000000000000966 ) ) ;
#34327=EDGE_CURVE ( 'NONE', #43290, #7311, #19844, .T. ) ;
#34333=ORIENTED_EDGE ( 'NONE', *, *, #7514, .F. ) ;
#34367=VERTEX_POINT ( 'NONE', #12438 ) ;
#34540=B_SPLINE_CURVE_WITH_KNOTS ( 'NONE', 3,
 ( #35051, #28412, #12889, #1315 ),
 .UNSPECIFIED., .F., .F.,
 ( 4, 4 ),
 ( 0.001041996463599131851, 0.002493317452641906698 ),
 .UNSPECIFIED. ) ;
#34598=CARTESIAN_POINT ( 'NONE',  ( -45.92409385541306222, -13.70421070448077039, 70.50000000000000000 ) ) ;
#34681=CARTESIAN_POINT ( 'NONE',  ( -45.92409385541306222, -14.20920654474410760, 70.50000000000000000 ) ) ;
#34697=DIRECTION ( 'NONE',  ( 1.224646799147353207E-16, 1.000000000000000000, -1.912410701131276611E-32 ) ) ;
#34844=DIRECTION ( 'NONE',  ( -2.160207931474222106E-15, -0.8949343913984794119, 0.4461977533473619473 ) ) ;
#34878=CARTESIAN_POINT ( 'NONE',  ( -45.92409385541306222, -14.38986189584960051, 70.50000000000000000 ) ) ;
#34929=ORIENTED_EDGE ( 'NONE', *, *, #25506, .F. ) ;
#34954=CARTESIAN_POINT ( 'NONE',  ( -45.92409385541306222, 12.69079345525585545, 70.50000000000000000 ) ) ;
#34961=B_SPLINE_CURVE_WITH_KNOTS ( 'NONE', 3,
 ( #47568, #13566, #13326, #39453 ),
 .UNSPECIFIED., .F., .F.,
 ( 4, 4 ),
 ( 0.001041996463599131851, 0.002493317452641904963 ),
 .UNSPECIFIED. ) ;
#34963=DIRECTION ( 'NONE',  ( 0.000000000000000000, 0.000000000000000000, 1.000000000000000000 ) ) ;
#35001=DIRECTION ( 'NONE',  ( 1.224646799147353207E-16, 1.000000000000000000, -1.912410701131276611E-32 ) ) ;
#35051=CARTESIAN_POINT ( 'NONE',  ( -46.29409385541305255, -12.76354662275040219, 69.95698270748289360 ) ) ;
#35059=CARTESIAN_POINT ( 'NONE',  ( -45.92409385541306932, -16.70920654474410938, 70.50000000000000000 ) ) ;
#35086=CARTESIAN_POINT ( 'NONE',  ( -45.55409385541306477, -12.70920654474410760, 71.79999999999999716 ) ) ;
#35097=EDGE_CURVE ( 'NONE', #27032, #47884, #27745, .T. ) ;
#35131=EDGE_LOOP ( 'NONE', ( #32640, #10097, #26040, #5234 ) ) ;
#35152=AXIS2_PLACEMENT_3D ( 'NONE', #36252, #13108, #13593 ) ;
#35166=CYLINDRICAL_SURFACE ( 'NONE', #19023, 1.250000000000001110 ) ;
#35171=EDGE_CURVE ( 'NONE', #43290, #39133, #20797, .T. ) ;
#35194=CIRCLE ( 'NONE', #42318, 0.09999999999999939493 ) ;
#35226=DIRECTION ( 'NONE',  ( 0.8949343913984055821, -0.4461977533475101620, -3.119193279067933041E-16 ) ) ;
#35259=DIRECTION ( 'NONE',  ( 6.695352868347749370E-17, -2.732354947069688554E-32, -1.000000000000000000 ) ) ;
#35325=( BOUNDED_CURVE ( )  B_SPLINE_CURVE ( 3, ( #43629, #39679, #36446, #47326 ),
 .UNSPECIFIED., .F., .F. ) 
 B_SPLINE_CURVE_WITH_KNOTS ( ( 4, 4 ),
 ( 6.147240100463205792, 6.283185307179586232 ),
 .UNSPECIFIED. ) 
 CURVE ( )  GEOMETRIC_REPRESENTATION_ITEM ( )  RATIONAL_B_SPLINE_CURVE ( ( 1.000000000000000000, 0.9984605012767906462, 0.9984605012767906462, 1.000000000000000000 ) ) 
 REPRESENTATION_ITEM ( '' )  );
#35329=CARTESIAN_POINT ( 'NONE',  ( -45.92409385541306222, -14.80920654474410902, 71.85000000000000853 ) ) ;
#35376=EDGE_LOOP ( 'NONE', ( #15852, #43884, #40363, #32652 ) ) ;
#35379=EDGE_LOOP ( 'NONE', ( #26416, #8936, #24767, #42104 ) ) ;
#35435=ORIENTED_EDGE ( 'NONE', *, *, #37886, .F. ) ;
#35481=CARTESIAN_POINT ( 'NONE',  ( -45.85858821786030859, -14.20920654474410760, 71.05212771298751306 ) ) ;
#35489=VERTEX_POINT ( 'NONE', #38119 ) ;
#35557=EDGE_CURVE ( 'NONE', #30449, #27032, #17648, .T. ) ;
#35613=ORIENTED_EDGE ( 'NONE', *, *, #22561, .F. ) ;
#35618=LINE ( 'NONE', #19652, #17283 ) ;
#35647=ORIENTED_EDGE ( 'NONE', *, *, #33310, .T. ) ;
#35672=DIRECTION ( 'NONE',  ( 1.224646799147353207E-16, 1.000000000000000000, -1.912410701131276611E-32 ) ) ;
#35708=VECTOR ( 'NONE', #25187, 1000.000000000000000 ) ;
#35714=SURFACE_STYLE_FILL_AREA ( #24663 ) ;
#35740=DIRECTION ( 'NONE',  ( -1.224646799147353207E-16, -1.000000000000000000, 1.935130192142698731E-16 ) ) ;
#35836=VERTEX_POINT ( 'NONE', #5022 ) ;
#35850=EDGE_CURVE ( 'NONE', #24736, #38529, #29433, .T. ) ;
#35962=DIRECTION ( 'NONE',  ( 1.224646799147353207E-16, 1.000000000000000000, -1.912410701131276611E-32 ) ) ;
#35988=VECTOR ( 'NONE', #18101, 1000.000000000000000 ) ;
#36007=DIRECTION ( 'NONE',  ( -3.484385612528001215E-15, 0.000000000000000000, 1.000000000000000000 ) ) ;
#36022=AXIS2_PLACEMENT_3D ( 'NONE', #30875, #12628, #41705 ) ;
#36092=ORIENTED_EDGE ( 'NONE', *, *, #40438, .T. ) ;
#36108=CARTESIAN_POINT ( 'NONE',  ( -45.92409385541306222, -14.20920654474410760, 70.50000000000000000 ) ) ;
#36119=ORIENTED_EDGE ( 'NONE', *, *, #7303, .T. ) ;
#36174=CLOSED_SHELL ( 'NONE', ( #40917, #8819, #39251, #14005, #21564, #24503, #78, #12257, #26049, #25267, #32184, #36792, #14079, #41238, #37845, #22127, #15659, #16642, #22727, #42577, #43213, #20726, #37901, #8747, #4109, #22631, #9564, #30229, #16143, #1971, #30123, #37133, #40700, #43668, #5818, #39906, #16873, #13781, #21922, #29564, #46164, #27624, #14739 ) ) ;
#36176=EDGE_CURVE ( 'NONE', #37218, #35836, #9833, .T. ) ;
#36245=CIRCLE ( 'NONE', #6375, 1.250000000000001110 ) ;
#36252=CARTESIAN_POINT ( 'NONE',  ( -45.92409385541306222, -13.51240245935757578, 70.50000000000000000 ) ) ;
#36334=CYLINDRICAL_SURFACE ( 'NONE', #132, 2.500000000000002220 ) ;
#36368=DIRECTION ( 'NONE',  ( -1.000000000000000000, 1.224646799147353207E-16, -4.267285103686820140E-17 ) ) ;
#36413=VECTOR ( 'NONE', #34844, 1000.000000000000000 ) ;
#36446=CARTESIAN_POINT ( 'NONE',  ( -45.94601335259982022, -14.20017296387473138, 71.05663168951065245 ) ) ;
#36495=ORIENTED_EDGE ( 'NONE', *, *, #38728, .F. ) ;
#36504=PLANE ( 'NONE',  #25700 ) ;
#36551=DIRECTION ( 'NONE',  ( 0.000000000000000000, 0.8949343913984796339, -0.4461977533473615032 ) ) ;
#36578=CARTESIAN_POINT ( 'NONE',  ( -45.37196614242555626, -14.20920654474410760, 70.56550563755274652 ) ) ;
#36582=FACE_OUTER_BOUND ( 'NONE', #39031, .T. ) ;
#36598=CARTESIAN_POINT ( 'NONE',  ( -45.92409385541306222, -14.20920654474410760, 71.05600000000001160 ) ) ;
#36640=CIRCLE ( 'NONE', #2084, 1.350000000000004086 ) ;
#36784=DIRECTION ( 'NONE',  ( 1.224646799147353207E-16, 1.000000000000000000, -1.912410701131276611E-32 ) ) ;
#36792=ADVANCED_FACE ( 'NONE', ( #22442 ), #7931, .T. ) ;
#36795=DIRECTION ( 'NONE',  ( 3.020324423671394676E-15, -0.4461977533473620028, -0.8949343913984795229 ) ) ;
#36841=DIRECTION ( 'NONE',  ( 1.260386242728853816E-16, 0.9975640502598247528, 0.06975647374411808599 ) ) ;
#36874=ORIENTED_EDGE ( 'NONE', *, *, #35097, .F. ) ;
#36950=ORIENTED_EDGE ( 'NONE', *, *, #7011, .F. ) ;
#36957=DIRECTION ( 'NONE',  ( 5.410999918679618404E-17, 0.000000000000000000, 1.000000000000000000 ) ) ;
#36991=DIRECTION ( 'NONE',  ( -1.224646799147353207E-16, -1.000000000000000000, 1.912410701131276611E-32 ) ) ;
#37102=DIRECTION ( 'NONE',  ( -0.8949343913984795229, -0.4461977533473618918, 4.967883834297468681E-17 ) ) ;
#37133=ADVANCED_FACE ( 'NONE', ( #7133 ), #3666, .T. ) ;
#37161=ORIENTED_EDGE ( 'NONE', *, *, #40346, .T. ) ;
#37173=EDGE_LOOP ( 'NONE', ( #35613, #19173, #25385, #37926 ) ) ;
#37218=VERTEX_POINT ( 'NONE', #33197 ) ;
#37271=CARTESIAN_POINT ( 'NONE',  ( -45.85858821786293049, -14.20920654474410760, 69.94787228701220272 ) ) ;
#37356=AXIS2_PLACEMENT_3D ( 'NONE', #44809, #40594, #29777 ) ;
#37375=DIRECTION ( 'NONE',  ( 0.000000000000000000, 0.000000000000000000, 1.000000000000000000 ) ) ;
#37389=ORIENTED_EDGE ( 'NONE', *, *, #36176, .F. ) ;
#37393=DIRECTION ( 'NONE',  ( 1.224646799147353207E-16, 1.000000000000000000, -1.912410701131276611E-32 ) ) ;
#37433=DIRECTION ( 'NONE',  ( 1.224646799147352961E-16, 1.000000000000000000, -5.292884291094200710E-16 ) ) ;
#37540=EDGE_CURVE ( 'NONE', #25382, #7068, #29414, .T. ) ;
#37604=ORIENTED_EDGE ( 'NONE', *, *, #33744, .F. ) ;
#37665=DIRECTION ( 'NONE',  ( -1.224646799147353207E-16, -1.000000000000000000, 1.912410701131276611E-32 ) ) ;
#37670=AXIS2_PLACEMENT_3D ( 'NONE', #184, #7564, #30221 ) ;
#37676=EDGE_LOOP ( 'NONE', ( #12133, #17937, #48269, #41242 ) ) ;
#37699=CARTESIAN_POINT ( 'NONE',  ( -45.92409385541306222, -14.20920654474410760, 70.50000000000000000 ) ) ;
#37717=CIRCLE ( 'NONE', #37670, 0.5560000000000009379 ) ;
#37724=AXIS2_PLACEMENT_3D ( 'NONE', #48453, #18408, #18914 ) ;
#37742=AXIS2_PLACEMENT_3D ( 'NONE', #6260, #13383, #43457 ) ;
#37777=EDGE_LOOP ( 'NONE', ( #40456, #434, #16994, #17110, #14398, #33980, #19860 ) ) ;
#37779=EDGE_CURVE ( 'NONE', #3121, #8094, #16833, .T. ) ;
#37787=CARTESIAN_POINT ( 'NONE',  ( -45.92409385541306222, -17.80920654474411435, 70.50000000000000000 ) ) ;
#37818=CIRCLE ( 'NONE', #29178, 2.404255319148937531 ) ;
#37845=ADVANCED_FACE ( 'NONE', ( #32339 ), #25905, .F. ) ;
#37849=VERTEX_POINT ( 'NONE', #6229 ) ;
#37886=EDGE_CURVE ( 'NONE', #22122, #27032, #6476, .T. ) ;
#37901=ADVANCED_FACE ( 'NONE', ( #21967 ), #40206, .T. ) ;
#37907=ORIENTED_EDGE ( 'NONE', *, *, #42657, .T. ) ;
#37913=VERTEX_POINT ( 'NONE', #13592 ) ;
#37926=ORIENTED_EDGE ( 'NONE', *, *, #35850, .F. ) ;
#37949=LINE ( 'NONE', #4236, #24243 ) ;
#38055=EDGE_LOOP ( 'NONE', ( #44425, #1127 ) ) ;
#38119=CARTESIAN_POINT ( 'NONE',  ( -43.51983853626412468, -13.51240245935757578, 70.50000000000000000 ) ) ;
#38132=ORIENTED_EDGE ( 'NONE', *, *, #12287, .F. ) ;
#38170=DIRECTION ( 'NONE',  ( 0.000000000000000000, 0.000000000000000000, 1.000000000000000000 ) ) ;
#38195=ORIENTED_EDGE ( 'NONE', *, *, #42754, .F. ) ;
#38199=EDGE_CURVE ( 'NONE', #32734, #40286, #45967, .T. ) ;
#38237=ORIENTED_EDGE ( 'NONE', *, *, #15928, .F. ) ;
#38398=CARTESIAN_POINT ( 'NONE',  ( -45.36800283045199933, -16.43194983366105077, 70.50000000000000000 ) ) ;
#38400=EDGE_LOOP ( 'NONE', ( #32500, #20760, #12567 ) ) ;
#38453=VECTOR ( 'NONE', #28565, 1000.000000000000227 ) ;
#38458=EDGE_LOOP ( 'NONE', ( #4366, #25706, #41775, #39096, #38237, #19618, #46786 ) ) ;
#38520=CIRCLE ( 'NONE', #17289, 0.6570903894995150374 ) ;
#38529=VERTEX_POINT ( 'NONE', #22844 ) ;
#38543=DIRECTION ( 'NONE',  ( 1.294152349642661695E-15, -0.8949343913984055821, -0.4461977533475101065 ) ) ;
#38562=LINE ( 'NONE', #42028, #25196 ) ;
#38659=ORIENTED_EDGE ( 'NONE', *, *, #46524, .F. ) ;
#38694=ORIENTED_EDGE ( 'NONE', *, *, #11699, .F. ) ;
#38728=EDGE_CURVE ( 'NONE', #40177, #41701, #31829, .T. ) ;
#38729=CARTESIAN_POINT ( 'NONE',  ( -45.92409385541306222, 12.69079345525585545, 69.25000000000000000 ) ) ;
#38758=VECTOR ( 'NONE', #22806, 1000.000000000000000 ) ;
#38841=PLANE ( 'NONE',  #45329 ) ;
#38900=VERTEX_POINT ( 'NONE', #15291 ) ;
#38927=AXIS2_PLACEMENT_3D ( 'NONE', #24539, #17595, #20593 ) ;
#38956=FACE_OUTER_BOUND ( 'NONE', #422, .T. ) ;
#39005=DIRECTION ( 'NONE',  ( -6.336017706050180129E-14, 0.000000000000000000, -1.000000000000000000 ) ) ;
#39026=VECTOR ( 'NONE', #16460, 1000.000000000000000 ) ;
#39031=EDGE_LOOP ( 'NONE', ( #23963, #34929 ) ) ;
#39043=CARTESIAN_POINT ( 'NONE',  ( -45.92409385541306932, -12.76354662275040042, 70.50000000000000000 ) ) ;
#39086=ORIENTED_EDGE ( 'NONE', *, *, #21805, .F. ) ;
#39096=ORIENTED_EDGE ( 'NONE', *, *, #22491, .F. ) ;
#39121=CARTESIAN_POINT ( 'NONE',  ( -45.92409385541306222, -14.80920654474410902, 70.50000000000000000 ) ) ;
#39133=VERTEX_POINT ( 'NONE', #16175 ) ;
#39236=CIRCLE ( 'NONE', #718, 2.500000000000002220 ) ;
#39251=ADVANCED_FACE ( 'NONE', ( #42562 ), #20832, .F. ) ;
#39307=VECTOR ( 'NONE', #36368, 1000.000000000000000 ) ;
#39338=CARTESIAN_POINT ( 'NONE',  ( -46.42632161746406894, -13.24559821555319061, 70.87000000000000455 ) ) ;
#39355=DIRECTION ( 'NONE',  ( 0.000000000000000000, 0.000000000000000000, 1.000000000000000000 ) ) ;
#39372=DIRECTION ( 'NONE',  ( 1.224646799147353207E-16, 1.000000000000000000, -1.912410701131276611E-32 ) ) ;
#39379=DIRECTION ( 'NONE',  ( 1.000000000000000000, 0.000000000000000000, 0.000000000000000000 ) ) ;
#39435=CARTESIAN_POINT ( 'NONE',  ( -45.92409385541306222, -13.51240245935757578, 70.50000000000000000 ) ) ;
#39453=CARTESIAN_POINT ( 'NONE',  ( -45.55409385541306477, -14.20920654474410760, 70.91501325280044910 ) ) ;
#39595=CARTESIAN_POINT ( 'NONE',  ( -45.92409385541306222, 12.69079345525585545, 70.50000000000000000 ) ) ;
#39609=CARTESIAN_POINT ( 'NONE',  ( -45.92409385541306222, 12.69079345525585545, 73.00000000000001421 ) ) ;
#39679=CARTESIAN_POINT ( 'NONE',  ( -45.96788223222966963, -14.20318880037429921, 71.05512804915051106 ) ) ;
#39689=DIRECTION ( 'NONE',  ( -1.000000000000000000, 0.000000000000000000, 0.000000000000000000 ) ) ;
#39701=DIRECTION ( 'NONE',  ( 1.224646799147353207E-16, 1.000000000000000000, -1.912410701131276611E-32 ) ) ;
#39770=VERTEX_POINT ( 'NONE', #18619 ) ;
#39866=CARTESIAN_POINT ( 'NONE',  ( -45.37196614242555626, -14.20920654474410760, 70.13000000000000966 ) ) ;
#39873=VECTOR ( 'NONE', #48328, 1000.000000000000000 ) ;
#39895=VERTEX_POINT ( 'NONE', #42517 ) ;
#39906=ADVANCED_FACE ( 'NONE', ( #6290 ), #47577, .F. ) ;
#39940=CARTESIAN_POINT ( 'NONE',  ( -46.29409385541305255, -13.72754205882879042, 70.96013658682592506 ) ) ;
#40019=CONICAL_SURFACE ( 'NONE', #14032, 0.5560000000000009379, 0.06981317007976595157 ) ;
#40026=AXIS2_PLACEMENT_3D ( 'NONE', #36108, #13694, #28739 ) ;
#40032=ORIENTED_EDGE ( 'NONE', *, *, #18820, .T. ) ;
#40046=CARTESIAN_POINT ( 'NONE',  ( -45.92409385541306222, 12.69079345525585545, 70.50000000000000000 ) ) ;
#40058=ORIENTED_EDGE ( 'NONE', *, *, #18703, .T. ) ;
#40083=CARTESIAN_POINT ( 'NONE',  ( -45.50908060261262023, -14.20920654474410760, 70.87000000000000455 ) ) ;
#40175=AXIS2_PLACEMENT_3D ( 'NONE', #17667, #24109, #20422 ) ;
#40177=VERTEX_POINT ( 'NONE', #46394 ) ;
#40199=CIRCLE ( 'NONE', #11871, 0.5560000000000009379 ) ;
#40206=PLANE ( 'NONE',  #6622 ) ;
#40232=AXIS2_PLACEMENT_3D ( 'NONE', #25380, #10598, #28823 ) ;
#40255=AXIS2_PLACEMENT_3D ( 'NONE', #17181, #13494, #28293 ) ;
#40286=VERTEX_POINT ( 'NONE', #20286 ) ;
#40307=CARTESIAN_POINT ( 'NONE',  ( -45.92409385541306222, 12.69079345525585545, 71.75000000000001421 ) ) ;
#40337=AXIS2_PLACEMENT_3D ( 'NONE', #13125, #24496, #20781 ) ;
#40346=EDGE_CURVE ( 'NONE', #37913, #11700, #14556, .T. ) ;
#40363=ORIENTED_EDGE ( 'NONE', *, *, #12287, .T. ) ;
#40438=EDGE_CURVE ( 'NONE', #8094, #28537, #10664, .T. ) ;
#40453=CARTESIAN_POINT ( 'NONE',  ( -45.92409385541306222, -14.20920654474410760, 71.05600000000001160 ) ) ;
#40456=ORIENTED_EDGE ( 'NONE', *, *, #4368, .F. ) ;
#40547=DIRECTION ( 'NONE',  ( 0.000000000000000000, 0.000000000000000000, 1.000000000000000000 ) ) ;
#40549=CARTESIAN_POINT ( 'NONE',  ( -45.37196614242555626, -14.20920654474410760, 70.87000000000000455 ) ) ;
#40594=DIRECTION ( 'NONE',  ( -1.224646799147353207E-16, -1.000000000000000000, 1.912410701131276611E-32 ) ) ;
#40608=( NAMED_UNIT ( * ) PLANE_ANGLE_UNIT ( ) SI_UNIT ( $, .RADIAN. ) );
#40610=DIRECTION ( 'NONE',  ( 2.342027643795563533E-48, 1.912410701131276611E-32, 1.000000000000000000 ) ) ;
#40679=DIRECTION ( 'NONE',  ( 1.224646799147353207E-16, 1.000000000000000000, -1.912410701131276611E-32 ) ) ;
#40700=ADVANCED_FACE ( 'NONE', ( #25600 ), #27191, .F. ) ;
#40723=CARTESIAN_POINT ( 'NONE',  ( -46.29409385541305966, -14.20920654474410760, 70.91501325280044910 ) ) ;
#40786=PLANE ( 'NONE',  #6971 ) ;
#40808=PLANE ( 'NONE',  #47670 ) ;
#40813=VECTOR ( 'NONE', #34015, 1000.000000000000000 ) ;
#40819=AXIS2_PLACEMENT_3D ( 'NONE', #16430, #2391, #9556 ) ;
#40834=PLANE ( 'NONE',  #34306 ) ;
#40901=CARTESIAN_POINT ( 'NONE',  ( -46.46711114793018282, -12.76354662275040219, 70.13000000000000966 ) ) ;
#40915=FACE_OUTER_BOUND ( 'NONE', #31073, .T. ) ;
#40917=ADVANCED_FACE ( 'NONE', ( #7887 ), #30368, .F. ) ;
#40977=CARTESIAN_POINT ( 'NONE',  ( -45.36595154876284397, -14.19714313411803985, 70.52197034960535404 ) ) ;
#40978=EDGE_LOOP ( 'NONE', ( #23077, #9511, #38694, #42040, #15868 ) ) ;
#41100=PLANE ( 'NONE',  #4738 ) ;
#41176=CARTESIAN_POINT ( 'NONE',  ( -45.92409385541306222, -14.20920654474410760, 70.50000000000000000 ) ) ;
#41195=PLANE ( 'NONE',  #13141 ) ;
#41197=VERTEX_POINT ( 'NONE', #29487 ) ;
#41238=ADVANCED_FACE ( 'NONE', ( #43797 ), #40808, .F. ) ;
#41242=ORIENTED_EDGE ( 'NONE', *, *, #48261, .T. ) ;
#41245=CARTESIAN_POINT ( 'NONE',  ( -46.29409385541305255, -14.20920654474410760, 69.94787228701220272 ) ) ;
#41366=PLANE ( 'NONE',  #24971 ) ;
#41371=AXIS2_PLACEMENT_3D ( 'NONE', #39121, #39372, #982 ) ;
#41393=DIRECTION ( 'NONE',  ( 4.267285103686815209E-17, -5.292884291094200710E-16, -1.000000000000000000 ) ) ;
#41397=CARTESIAN_POINT ( 'NONE',  ( -45.92409385541306222, -14.90920654474410867, 69.15000000000000568 ) ) ;
#41422=CARTESIAN_POINT ( 'NONE',  ( -47.22409385541305937, -12.70920654474410760, 70.13000000000000966 ) ) ;
#41469=ORIENTED_EDGE ( 'NONE', *, *, #4246, .F. ) ;
#41519=LINE ( 'NONE', #10999, #23678 ) ;
#41576=VERTEX_POINT ( 'NONE', #14553 ) ;
#41644=CARTESIAN_POINT ( 'NONE',  ( -45.42186609336205549, -13.24559821555319239, 70.13000000000000966 ) ) ;
#41701=VERTEX_POINT ( 'NONE', #30605 ) ;
#41705=DIRECTION ( 'NONE',  ( -5.551115123125782702E-17, -1.232595164407830946E-32, -1.000000000000000000 ) ) ;
#41739=PRODUCT_DEFINITION_SHAPE ( 'NONE', 'NONE',  #9649 ) ;
#41744=FACE_OUTER_BOUND ( 'NONE', #29807, .T. ) ;
#41775=ORIENTED_EDGE ( 'NONE', *, *, #11533, .F. ) ;
#41779=ORIENTED_EDGE ( 'NONE', *, *, #11699, .T. ) ;
#41810=AXIS2_PLACEMENT_3D ( 'NONE', #27548, #11810, #18945 ) ;
#42001=CARTESIAN_POINT ( 'NONE',  ( -45.92409385541306222, -14.80920654474410902, 73.00000000000001421 ) ) ;
#42024=DIRECTION ( 'NONE',  ( -1.224646799147353207E-16, -1.000000000000000000, 1.912410701131276611E-32 ) ) ;
#42028=CARTESIAN_POINT ( 'NONE',  ( -46.29409385541305966, -14.20920654474410760, 71.05212771298751306 ) ) ;
#42040=ORIENTED_EDGE ( 'NONE', *, *, #45982, .F. ) ;
#42069=UNCERTAINTY_MEASURE_WITH_UNIT (LENGTH_MEASURE( 1.000000000000000082E-05 ), #14481, 'distance_accuracy_value', 'NONE');
#42104=ORIENTED_EDGE ( 'NONE', *, *, #10977, .F. ) ;
#42142=EDGE_CURVE ( 'NONE', #28374, #40286, #42826, .T. ) ;
#42199=CARTESIAN_POINT ( 'NONE',  ( -45.42186609336205549, -13.24559821555319239, 70.87000000000000455 ) ) ;
#42276=ORIENTED_EDGE ( 'NONE', *, *, #11093, .F. ) ;
#42313=AXIS2_PLACEMENT_3D ( 'NONE', #26059, #15683, #45034 ) ;
#42318=AXIS2_PLACEMENT_3D ( 'NONE', #41397, #6700, #29102 ) ;
#42360=ORIENTED_EDGE ( 'NONE', *, *, #45086, .T. ) ;
#42420=AXIS2_PLACEMENT_3D ( 'NONE', #45105, #17987, #10622 ) ;
#42448=DIRECTION ( 'NONE',  ( 0.000000000000000000, -1.000000000000000000, 0.000000000000000000 ) ) ;
#42449=CARTESIAN_POINT ( 'NONE',  ( -46.47622156840087371, -14.20920654474410760, 70.13000000000000966 ) ) ;
#42461=EDGE_CURVE ( 'NONE', #28350, #32762, #31197, .T. ) ;
#42497=SHAPE_DEFINITION_REPRESENTATION ( #41739, #11272 ) ;
#42517=CARTESIAN_POINT ( 'NONE',  ( -45.92409385541306222, -14.90920654474410867, 69.25000000000000000 ) ) ;
#42562=FACE_OUTER_BOUND ( 'NONE', #37173, .T. ) ;
#42577=ADVANCED_FACE ( 'NONE', ( #16076 ), #45186, .F. ) ;
#42609=ORIENTED_EDGE ( 'NONE', *, *, #47583, .T. ) ;
#42657=EDGE_CURVE ( 'NONE', #10249, #2125, #28052, .T. ) ;
#42710=CARTESIAN_POINT ( 'NONE',  ( -45.85858821786030859, -14.20920654474410760, 71.05212771298751306 ) ) ;
#42754=EDGE_CURVE ( 'NONE', #41701, #45322, #31998, .T. ) ;
#42802=VECTOR ( 'NONE', #47885, 1000.000000000000000 ) ;
#42815=FACE_OUTER_BOUND ( 'NONE', #37676, .T. ) ;
#42826=LINE ( 'NONE', #39609, #39026 ) ;
#43026=CARTESIAN_POINT ( 'NONE',  ( -45.92409385541306222, -14.90920654474410867, 70.50000000000000000 ) ) ;
#43080=CYLINDRICAL_SURFACE ( 'NONE', #13191, 1.250000000000001110 ) ;
#43115=EDGE_CURVE ( 'NONE', #31776, #7068, #12422, .T. ) ;
#43131=EDGE_LOOP ( 'NONE', ( #27229, #10959, #11889 ) ) ;
#43146=EDGE_LOOP ( 'NONE', ( #42360, #3110, #29233 ) ) ;
#43187=CARTESIAN_POINT ( 'NONE',  ( -48.32834917456199975, -13.51240245935757578, 70.50000000000000000 ) ) ;
#43213=ADVANCED_FACE ( 'NONE', ( #21523 ), #36504, .F. ) ;
#43229=FACE_OUTER_BOUND ( 'NONE', #35376, .T. ) ;
#43238=ORIENTED_EDGE ( 'NONE', *, *, #19020, .T. ) ;
#43264=CONICAL_SURFACE ( 'NONE', #16488, 0.5560000000000009379, 0.06981317007976595157 ) ;
#43265=ORIENTED_EDGE ( 'NONE', *, *, #35097, .T. ) ;
#43290=VERTEX_POINT ( 'NONE', #15806 ) ;
#43304=B_SPLINE_CURVE_WITH_KNOTS ( 'NONE', 3,
 ( #14288, #39940, #2984, #10628 ),
 .UNSPECIFIED., .F., .F.,
 ( 4, 4 ),
 ( 0.001310108020964425440, 0.002761379516307286858 ),
 .UNSPECIFIED. ) ;
#43408=PLANE ( 'NONE',  #18773 ) ;
#43457=DIRECTION ( 'NONE',  ( 0.000000000000000000, 0.000000000000000000, 1.000000000000000000 ) ) ;
#43479=DIRECTION ( 'NONE',  ( 1.224646799147353207E-16, 1.000000000000000000, -1.912410701131276611E-32 ) ) ;
#43629=CARTESIAN_POINT ( 'NONE',  ( -45.98959949296581584, -14.20920654474410760, 71.05212771298751306 ) ) ;
#43637=EDGE_LOOP ( 'NONE', ( #16601, #16830, #25789, #15768 ) ) ;
#43664=FACE_OUTER_BOUND ( 'NONE', #33429, .T. ) ;
#43668=ADVANCED_FACE ( 'NONE', ( #48508 ), #41366, .F. ) ;
#43689=CARTESIAN_POINT ( 'NONE',  ( -45.92409385541306932, -12.76354662275040042, 70.50000000000000000 ) ) ;
#43716=ORIENTED_EDGE ( 'NONE', *, *, #18703, .F. ) ;
#43750=FACE_OUTER_BOUND ( 'NONE', #20544, .T. ) ;
#43797=FACE_OUTER_BOUND ( 'NONE', #38458, .T. ) ;
#43884=ORIENTED_EDGE ( 'NONE', *, *, #5321, .F. ) ;
#43966=AXIS2_PLACEMENT_3D ( 'NONE', #15051, #3258, #25658 ) ;
#43987=CARTESIAN_POINT ( 'NONE',  ( -45.92409385541306222, -14.20920654474410760, 70.50000000000000000 ) ) ;
#44293=CARTESIAN_POINT ( 'NONE',  ( -45.55409385541305767, -14.20920654474410760, 69.94787228701220272 ) ) ;
#44313=EDGE_CURVE ( 'NONE', #32762, #44898, #2184, .T. ) ;
#44320=EDGE_CURVE ( 'NONE', #19297, #32762, #8486, .T. ) ;
#44390=ORIENTED_EDGE ( 'NONE', *, *, #44465, .F. ) ;
#44425=ORIENTED_EDGE ( 'NONE', *, *, #6120, .T. ) ;
#44431=LINE ( 'NONE', #7250, #30838 ) ;
#44447=ORIENTED_EDGE ( 'NONE', *, *, #27935, .F. ) ;
#44465=EDGE_CURVE ( 'NONE', #16407, #73, #3093, .T. ) ;
#44499=CARTESIAN_POINT ( 'NONE',  ( -45.37196614242555626, -14.20920654474410760, 70.13000000000000966 ) ) ;
#44568=DIRECTION ( 'NONE',  ( 0.000000000000000000, 0.000000000000000000, 1.000000000000000000 ) ) ;
#44578=EDGE_CURVE ( 'NONE', #10249, #38900, #26591, .T. ) ;
#44608=CARTESIAN_POINT ( 'NONE',  ( -46.38423044223897307, -13.72754205882879042, 70.13000000000000966 ) ) ;
#44704=EDGE_LOOP ( 'NONE', ( #10122, #391, #3910, #19017, #8838, #9258, #40058, #27731, #9935, #36092, #45058 ) ) ;
#44796=CARTESIAN_POINT ( 'NONE',  ( -45.90212350580859635, -14.19714313411900264, 69.94185769334995939 ) ) ;
#44809=CARTESIAN_POINT ( 'NONE',  ( -44.67409385541305511, -17.80920654474411435, 70.50000000000000000 ) ) ;
#44855=CARTESIAN_POINT ( 'NONE',  ( -45.98959949296581584, -14.20920654474410760, 71.05212771298751306 ) ) ;
#44898=VERTEX_POINT ( 'NONE', #4946 ) ;
#45003=ORIENTED_EDGE ( 'NONE', *, *, #37886, .T. ) ;
#45017=VERTEX_POINT ( 'NONE', #17925 ) ;
#45034=DIRECTION ( 'NONE',  ( 0.000000000000000000, 0.000000000000000000, 1.000000000000000000 ) ) ;
#45050=CARTESIAN_POINT ( 'NONE',  ( -45.98959949296318683, -14.20920654474410760, 69.94787228701220272 ) ) ;
#45058=ORIENTED_EDGE ( 'NONE', *, *, #7604, .T. ) ;
#45086=EDGE_CURVE ( 'NONE', #19297, #44898, #25076, .T. ) ;
#45105=CARTESIAN_POINT ( 'NONE',  ( -45.92409385541306222, -14.20920654474410760, 70.50000000000000000 ) ) ;
#45129=FACE_OUTER_BOUND ( 'NONE', #40978, .T. ) ;
#45186=PLANE ( 'NONE',  #2883 ) ;
#45203=AXIS2_PLACEMENT_3D ( 'NONE', #3661, #30522, #37375 ) ;
#45237=CARTESIAN_POINT ( 'NONE',  ( -44.67409385541305511, -14.80920654474410725, 70.50000000000000000 ) ) ;
#45301=DIRECTION ( 'NONE',  ( 0.000000000000000000, 0.000000000000000000, 1.000000000000000000 ) ) ;
#45322=VERTEX_POINT ( 'NONE', #13453 ) ;
#45329=AXIS2_PLACEMENT_3D ( 'NONE', #27279, #461, #23346 ) ;
#45473=DIRECTION ( 'NONE',  ( 1.224646799147353207E-16, 1.000000000000000000, -1.912410701131276611E-32 ) ) ;
#45510=CIRCLE ( 'NONE', #15598, 1.250000000000001110 ) ;
#45602=CARTESIAN_POINT ( 'NONE',  ( -45.38107656289594161, -12.76354662275040219, 70.13000000000000966 ) ) ;
#45622=DIRECTION ( 'NONE',  ( 0.000000000000000000, 0.000000000000000000, 1.000000000000000000 ) ) ;
#45625=CIRCLE ( 'NONE', #18056, 0.5560000000000009379 ) ;
#45756=STYLED_ITEM ( 'NONE', ( #2714 ), #31971 ) ;
#45766=AXIS2_PLACEMENT_3D ( 'NONE', #35059, #16339, #2305 ) ;
#45803=EDGE_CURVE ( 'NONE', #17364, #10113, #20366, .T. ) ;
#45903=DIRECTION ( 'NONE',  ( -1.224646799147353207E-16, -1.000000000000000000, 1.912410701131276611E-32 ) ) ;
#45942=CARTESIAN_POINT ( 'NONE',  ( -46.29409385541305255, -12.70920654474410760, 69.20000000000001705 ) ) ;
#45967=CIRCLE ( 'NONE', #3489, 2.500000000000002220 ) ;
#45982=EDGE_CURVE ( 'NONE', #2125, #35489, #25845, .T. ) ;
#46082=PRODUCT ( 'Attachment Screw', 'Attachment Screw', '', ( #4106 ) ) ;
#46118=CARTESIAN_POINT ( 'NONE',  ( -45.55409385541305767, -14.20920654474410760, 70.08498674719956512 ) ) ;
#46164=ADVANCED_FACE ( 'NONE', ( #4512 ), #40019, .F. ) ;
#46264=DIRECTION ( 'NONE',  ( 1.224646799147353207E-16, 1.000000000000000000, -1.912410701131276611E-32 ) ) ;
#46273=CIRCLE ( 'NONE', #11679, 2.500000000000002220 ) ;
#46320=ORIENTED_EDGE ( 'NONE', *, *, #48395, .F. ) ;
#46394=CARTESIAN_POINT ( 'NONE',  ( -46.46711114793018282, -12.76354662275040042, 70.87000000000000455 ) ) ;
#46397=CARTESIAN_POINT ( 'NONE',  ( -45.88030547859645480, -14.20318880037429565, 71.05512804915051106 ) ) ;
#46424=CIRCLE ( 'NONE', #6346, 0.5560000000000009379 ) ;
#46447=EDGE_LOOP ( 'NONE', ( #21627, #3604, #17573, #36950, #4549, #5846, #12165 ) ) ;
#46454=DIRECTION ( 'NONE',  ( 1.056002951008363407E-14, 0.000000000000000000, -1.000000000000000000 ) ) ;
#46465=CARTESIAN_POINT ( 'NONE',  ( -45.92409385541306222, -14.90920654474410867, 70.50000000000000000 ) ) ;
#46524=EDGE_CURVE ( 'NONE', #8094, #41701, #43304, .T. ) ;
#46630=DIRECTION ( 'NONE',  ( -1.224646799147353207E-16, -1.000000000000000000, 1.912410701131276611E-32 ) ) ;
#46691=DIRECTION ( 'NONE',  ( 1.224646799147353207E-16, 1.000000000000000000, -1.912410701131276611E-32 ) ) ;
#46725=VERTEX_POINT ( 'NONE', #20452 ) ;
#46777=ORIENTED_EDGE ( 'NONE', *, *, #11919, .F. ) ;
#46783=EDGE_CURVE ( 'NONE', #48327, #14597, #7814, .T. ) ;
#46786=ORIENTED_EDGE ( 'NONE', *, *, #29449, .F. ) ;
#46855=ORIENTED_EDGE ( 'NONE', *, *, #10170, .F. ) ;
#46875=CARTESIAN_POINT ( 'NONE',  ( -45.92409385541306222, -14.20017296387473316, 71.05663168951063824 ) ) ;
#46947=CARTESIAN_POINT ( 'NONE',  ( -45.92409385541306222, -14.20920654474410760, 70.50000000000000000 ) ) ;
#46984=DIRECTION ( 'NONE',  ( 1.224646799147353207E-16, 1.000000000000000000, -1.912410701131276611E-32 ) ) ;
#47060=EDGE_CURVE ( 'NONE', #7630, #37913, #8602, .T. ) ;
#47089=CARTESIAN_POINT ( 'NONE',  ( -45.92409385541306222, 12.69079345525585545, 68.00000000000000000 ) ) ;
#47096=CARTESIAN_POINT ( 'NONE',  ( -46.29409385541305966, -14.20920654474410760, 71.05212771298751306 ) ) ;
#47119=CONICAL_SURFACE ( 'NONE', #7800, 0.5560000000000009379, 0.06981317007976595157 ) ;
#47160=CARTESIAN_POINT ( 'NONE',  ( -45.92409385541306222, -13.51240245935757578, 72.90425531914894464 ) ) ;
#47170=DIRECTION ( 'NONE',  ( 0.000000000000000000, 0.000000000000000000, 1.000000000000000000 ) ) ;
#47212=AXIS2_PLACEMENT_3D ( 'NONE', #23403, #5173, #12552 ) ;
#47326=CARTESIAN_POINT ( 'NONE',  ( -45.92409385541306222, -14.20017296387473316, 71.05663168951063824 ) ) ;
#47368=CARTESIAN_POINT ( 'NONE',  ( -47.12338083056222615, -12.91120565595569758, 70.87000000000000455 ) ) ;
#47410=LINE ( 'NONE', #47642, #23757 ) ;
#47414=CARTESIAN_POINT ( 'NONE',  ( -45.55409385541305767, -14.20920654474410760, 69.94787228701220272 ) ) ;
#47418=DIRECTION ( 'NONE',  ( 1.224646799147353207E-16, 1.000000000000000000, -1.912410701131276611E-32 ) ) ;
#47444=CARTESIAN_POINT ( 'NONE',  ( -45.92409385541306222, -14.20920654474410760, 70.50000000000000000 ) ) ;
#47548=( LENGTH_UNIT ( ) NAMED_UNIT ( * ) SI_UNIT ( .MILLI., .METRE. ) );
#47568=CARTESIAN_POINT ( 'NONE',  ( -45.55409385541306477, -12.76354662275040397, 71.04301729251712061 ) ) ;
#47577=CONICAL_SURFACE ( 'NONE', #38927, 0.5560000000000009379, 0.06981317007976595157 ) ;
#47583=EDGE_CURVE ( 'NONE', #28350, #12407, #37949, .T. ) ;
#47596=CARTESIAN_POINT ( 'NONE',  ( -46.47622156840087371, -14.20920654474410760, 70.13000000000000966 ) ) ;
#47614=AXIS2_PLACEMENT_3D ( 'NONE', #18444, #37393, #40610 ) ;
#47642=CARTESIAN_POINT ( 'NONE',  ( -45.37196614242555626, -14.20920654474410760, 70.87000000000000455 ) ) ;
#47670=AXIS2_PLACEMENT_3D ( 'NONE', #22110, #37102, #10054 ) ;
#47672=DIRECTION ( 'NONE',  ( 0.000000000000000000, 0.000000000000000000, 1.000000000000000000 ) ) ;
#47838=EDGE_LOOP ( 'NONE', ( #45003, #43265, #2912, #24996 ) ) ;
#47884=VERTEX_POINT ( 'NONE', #963 ) ;
#47885=DIRECTION ( 'NONE',  ( -3.534154189880001717E-15, 4.519331686442879103E-31, 1.000000000000000000 ) ) ;
#47892=FACE_OUTER_BOUND ( 'NONE', #43131, .T. ) ;
#47897=CARTESIAN_POINT ( 'NONE',  ( -45.92409385541306222, -17.80920654474411435, 71.75000000000001421 ) ) ;
#47911=ORIENTED_EDGE ( 'NONE', *, *, #17378, .T. ) ;
#47983=VECTOR ( 'NONE', #39701, 1000.000000000000000 ) ;
#48063=AXIS2_PLACEMENT_3D ( 'NONE', #1450, #15976, #1707 ) ;
#48147=DIRECTION ( 'NONE',  ( 1.000000000000000000, -6.517531090241554163E-16, 3.534154189880001717E-15 ) ) ;
#48186=EDGE_CURVE ( 'NONE', #25382, #18791, #17176, .T. ) ;
#48261=EDGE_CURVE ( 'NONE', #38529, #39895, #45510, .T. ) ;
#48269=ORIENTED_EDGE ( 'NONE', *, *, #7584, .T. ) ;
#48294=ORIENTED_EDGE ( 'NONE', *, *, #7514, .T. ) ;
#48297=DIRECTION ( 'NONE',  ( 0.000000000000000000, 0.000000000000000000, 1.000000000000000000 ) ) ;
#48300=DIRECTION ( 'NONE',  ( -5.551115123125782702E-17, -1.232595164407830946E-32, -1.000000000000000000 ) ) ;
#48302=AXIS2_PLACEMENT_3D ( 'NONE', #1306, #8964, #5026 ) ;
#48306=LINE ( 'NONE', #4001, #40813 ) ;
#48327=VERTEX_POINT ( 'NONE', #47368 ) ;
#48328=DIRECTION ( 'NONE',  ( 1.000000000000000000, -1.224646799147353207E-16, 4.267285103686821372E-17 ) ) ;
#48330=AXIS2_PLACEMENT_3D ( 'NONE', #43026, #20630, #9790 ) ;
#48352=CARTESIAN_POINT ( 'NONE',  ( -45.37196614242555626, -14.20920654474410760, 70.56550563755274652 ) ) ;
#48358=ORIENTED_EDGE ( 'NONE', *, *, #24775, .F. ) ;
#48395=EDGE_CURVE ( 'NONE', #27032, #39770, #4613, .T. ) ;
#48410=DIRECTION ( 'NONE',  ( 0.000000000000000000, 0.000000000000000000, 1.000000000000000000 ) ) ;
#48453=CARTESIAN_POINT ( 'NONE',  ( -46.29409385541305255, -14.20920654474410760, 69.94787228701220272 ) ) ;
#48464=ADVANCED_BREP_SHAPE_REPRESENTATION ( '', ( #31971, #29031 ), #23534 ) ;
#48508=FACE_OUTER_BOUND ( 'NONE', #24544, .T. ) ;
#48527=DIRECTION ( 'NONE',  ( -0.8949343913984795229, -0.4461977533473618918, 4.967883834297468681E-17 ) ) ;
#48582=AXIS2_PLACEMENT_3D ( 'NONE', #32062, #35259, #39689 ) ;
#48656=FACE_OUTER_BOUND ( 'NONE', #30254, .T. ) ;
#48692=AXIS2_PLACEMENT_3D ( 'NONE', #16857, #11194, #118 ) ;
#48712=DIRECTION ( 'NONE',  ( -1.000000000000000000, 3.159776991290051445E-16, -3.534154189880001717E-15 ) ) ;
ENDSEC;
END-ISO-10303-21;
